ISO-10303-21;
HEADER;
FILE_DESCRIPTION (('STEP AP214'),
    '1' );
FILE_NAME ('Part6.step',
    '2026-11-01T05:08:46',
    ( '' ),
    ( '' ),
    'SwSTEP 2.0',
    'SolidWorks 2024',
    '' );
FILE_SCHEMA (( 'AUTOMOTIVE_DESIGN' ));
ENDSEC;

DATA;
#2=DIRECTION ( 'NONE',  ( 1.000000000000000000, 0.000000000000000000, 0.000000000000000000 ) ) ;
#6=CARTESIAN_POINT ( 'NONE',  ( 55.99999999999989342, 523.2161522479888163, -507.5890438806159750 ) ) ;
#7=ORIENTED_EDGE ( 'NONE', *, *, #1395, .F. ) ;
#21=VERTEX_POINT ( 'NONE', #5050 ) ;
#24=ORIENTED_EDGE ( 'NONE', *, *, #4784, .T. ) ;
#36=CIRCLE ( 'NONE', #12381, 84.99999999999997158 ) ;
#40=DIRECTION ( 'NONE',  ( 1.000000000000000000, 0.000000000000000000, 0.000000000000000000 ) ) ;
#41=EDGE_LOOP ( 'NONE', ( #1382, #8433, #6479, #15519 ) ) ;
#43=ORIENTED_EDGE ( 'NONE', *, *, #5912, .T. ) ;
#50=FACE_OUTER_BOUND ( 'NONE', #13064, .T. ) ;
#54=DIRECTION ( 'NONE',  ( 0.000000000000000000, 0.000000000000000000, -1.000000000000000000 ) ) ;
#71=VECTOR ( 'NONE', #2, 1000.000000000000000 ) ;
#72=CARTESIAN_POINT ( 'NONE',  ( -46.99999999999988631, 493.2350855268092573, -580.5705369404290650 ) ) ;
#78=DIRECTION ( 'NONE',  ( -1.000000000000000000, 0.000000000000000000, 0.000000000000000000 ) ) ;
#79=ORIENTED_EDGE ( 'NONE', *, *, #8581, .F. ) ;
#80=CARTESIAN_POINT ( 'NONE',  ( -46.99999999999988631, 523.2161522479888163, -502.8936384967199729 ) ) ;
#85=CYLINDRICAL_SURFACE ( 'NONE', #16920, 13.69540538389601991 ) ;
#102=EDGE_LOOP ( 'NONE', ( #5249, #13534 ) ) ;
#104=DIRECTION ( 'NONE',  ( 1.000000000000000000, 0.000000000000000000, 0.000000000000000000 ) ) ;
#108=PLANE ( 'NONE',  #4503 ) ;
#110=ORIENTED_EDGE ( 'NONE', *, *, #957, .T. ) ;
#116=AXIS2_PLACEMENT_3D ( 'NONE', #10320, #2489, #3792 ) ;
#118=CARTESIAN_POINT ( 'NONE',  ( 55.99999999999989342, 493.2350855268086320, -503.4847040861888559 ) ) ;
#124=ORIENTED_EDGE ( 'NONE', *, *, #2973, .T. ) ;
#130=ORIENTED_EDGE ( 'NONE', *, *, #10730, .F. ) ;
#132=ORIENTED_EDGE ( 'NONE', *, *, #8673, .T. ) ;
#134=AXIS2_PLACEMENT_3D ( 'NONE', #15085, #13801, #7423 ) ;
#136=EDGE_LOOP ( 'NONE', ( #13125, #124, #7060, #6376 ) ) ;
#151=AXIS2_PLACEMENT_3D ( 'NONE', #9424, #3927, #10623 ) ;
#158=DIRECTION ( 'NONE',  ( 1.000000000000000000, 0.000000000000000000, 0.000000000000000000 ) ) ;
#162=CIRCLE ( 'NONE', #11396, 13.69540538389601991 ) ;
#164=CARTESIAN_POINT ( 'NONE',  ( 175.0000000000000568, 515.4878487013597805, -546.7230258972048205 ) ) ;
#167=EDGE_CURVE ( 'NONE', #13498, #8853, #6611, .T. ) ;
#173=DIRECTION ( 'NONE',  ( -1.000000000000000000, -0.000000000000000000, 0.000000000000000000 ) ) ;
#174=CARTESIAN_POINT ( 'NONE',  ( -46.99999999999988631, 473.6663340069158039, -557.2494070140132862 ) ) ;
#177=DIRECTION ( 'NONE',  ( 0.000000000000000000, 0.000000000000000000, 1.000000000000000000 ) ) ;
#179=CARTESIAN_POINT ( 'NONE',  ( -49.99999999999999289, 515.4878487013597805, -546.7230258972048205 ) ) ;
#180=FACE_OUTER_BOUND ( 'NONE', #4687, .T. ) ;
#182=CARTESIAN_POINT ( 'NONE',  ( 55.99999999999989342, 523.2161522479893847, -590.5524132976893270 ) ) ;
#193=EDGE_CURVE ( 'NONE', #6600, #1481, #12667, .T. ) ;
#220=CARTESIAN_POINT ( 'NONE',  ( -46.99999999999988631, 559.9933750504617365, -546.7230258972048205 ) ) ;
#226=DIRECTION ( 'NONE',  ( -1.000000000000000000, -0.000000000000000000, 0.000000000000000000 ) ) ;
#230=DIRECTION ( 'NONE',  ( 0.000000000000000000, 0.3420201433256759294, -0.9396926207859057634 ) ) ;
#235=CARTESIAN_POINT ( 'NONE',  ( 55.99999999999989342, 493.2350855268086320, -508.1801094700848580 ) ) ;
#241=EDGE_CURVE ( 'NONE', #13085, #1073, #5982, .T. ) ;
#247=AXIS2_PLACEMENT_3D ( 'NONE', #6243, #15452, #15365 ) ;
#252=DIRECTION ( 'NONE',  ( 1.000000000000000000, -0.000000000000000000, 0.000000000000000000 ) ) ;
#253=DIRECTION ( 'NONE',  ( 0.000000000000000000, 0.000000000000000000, -1.000000000000000000 ) ) ;
#254=CARTESIAN_POINT ( 'NONE',  ( 55.99999999999989342, 473.6663340069158039, -561.9448123979092315 ) ) ;
#261=CARTESIAN_POINT ( 'NONE',  ( -45.00000000000000000, 515.4878487013597805, -546.7230258972048205 ) ) ;
#262=CARTESIAN_POINT ( 'NONE',  ( -55.99999999999989342, 549.5810598491749488, -561.6352214130889706 ) ) ;
#266=ORIENTED_EDGE ( 'NONE', *, *, #13819, .T. ) ;
#270=ORIENTED_EDGE ( 'NONE', *, *, #4582, .F. ) ;
#273=CARTESIAN_POINT ( 'NONE',  ( -45.00000000000000000, 549.5810598491746077, -531.8108303813202156 ) ) ;
#274=ORIENTED_EDGE ( 'NONE', *, *, #7860, .T. ) ;
#280=EDGE_CURVE ( 'NONE', #3951, #1946, #14054, .T. ) ;
#286=EDGE_CURVE ( 'NONE', #14252, #13943, #15423, .T. ) ;
#288=ORIENTED_EDGE ( 'NONE', *, *, #4993, .T. ) ;
#293=CARTESIAN_POINT ( 'NONE',  ( 46.99999999999988631, 523.2161522479893847, -604.2478186815853860 ) ) ;
#294=DIRECTION ( 'NONE',  ( 1.000000000000000000, 0.000000000000000000, 0.000000000000000000 ) ) ;
#302=ORIENTED_EDGE ( 'NONE', *, *, #11387, .T. ) ;
#305=ORIENTED_EDGE ( 'NONE', *, *, #6249, .T. ) ;
#307=ORIENTED_EDGE ( 'NONE', *, *, #286, .F. ) ;
#308=CARTESIAN_POINT ( 'NONE',  ( 55.99999999999989342, 523.2161522479888163, -516.5890438806160319 ) ) ;
#314=AXIS2_PLACEMENT_3D ( 'NONE', #72, #14498, #7952 ) ;
#320=DIRECTION ( 'NONE',  ( -1.000000000000000000, 0.000000000000000000, -0.000000000000000000 ) ) ;
#327=FACE_OUTER_BOUND ( 'NONE', #16316, .T. ) ;
#330=VECTOR ( 'NONE', #13966, 1000.000000000000000 ) ;
#339=CARTESIAN_POINT ( 'NONE',  ( 45.00000000000000000, 559.9933750504617365, -533.0276205133087615 ) ) ;
#340=ORIENTED_EDGE ( 'NONE', *, *, #12230, .T. ) ;
#354=AXIS2_PLACEMENT_3D ( 'NONE', #9251, #2799, #13200 ) ;
#360=ORIENTED_EDGE ( 'NONE', *, *, #4262, .F. ) ;
#361=ORIENTED_EDGE ( 'NONE', *, *, #4535, .F. ) ;
#383=EDGE_LOOP ( 'NONE', ( #13190, #2417, #10435, #10848 ) ) ;
#389=CARTESIAN_POINT ( 'NONE',  ( -55.99999999999989342, 549.5810598491749488, -580.0260321808809749 ) ) ;
#392=AXIS2_PLACEMENT_3D ( 'NONE', #3542, #12730, #15386 ) ;
#399=AXIS2_PLACEMENT_3D ( 'NONE', #3157, #5967, #8549 ) ;
#401=AXIS2_PLACEMENT_3D ( 'NONE', #16893, #5208, #2559 ) ;
#405=CARTESIAN_POINT ( 'NONE',  ( -55.99999999999989342, 473.6663340069157471, -545.1966447803968094 ) ) ;
#407=ADVANCED_FACE ( 'NONE', ( #5026 ), #16709, .T. ) ;
#410=DIRECTION ( 'NONE',  ( -1.000000000000000000, -0.000000000000000000, -0.000000000000000000 ) ) ;
#411=TOROIDAL_SURFACE ( 'NONE', #5329, 4.695405383895982609, 9.000000000000000000 ) ;
#415=CARTESIAN_POINT ( 'NONE',  ( -46.99999999999988631, 559.9933750504617365, -551.4184312811007658 ) ) ;
#416=AXIS2_PLACEMENT_3D ( 'NONE', #12043, #453, #4135 ) ;
#427=DIRECTION ( 'NONE',  ( -1.000000000000000000, 0.000000000000000000, 0.000000000000000000 ) ) ;
#430=DIRECTION ( 'NONE',  ( 1.000000000000000000, 0.000000000000000000, -0.000000000000000000 ) ) ;
#437=DIRECTION ( 'NONE',  ( -1.000000000000000000, 0.000000000000000000, 0.000000000000000000 ) ) ;
#441=ADVANCED_FACE ( 'NONE', ( #14401 ), #16961, .T. ) ;
#442=DIRECTION ( 'NONE',  ( 0.000000000000000000, 1.000000000000000000, -1.224646799147353207E-16 ) ) ;
#443=ORIENTED_EDGE ( 'NONE', *, *, #10669, .T. ) ;
#447=ORIENTED_EDGE ( 'NONE', *, *, #14022, .T. ) ;
#453=DIRECTION ( 'NONE',  ( -1.000000000000000000, 0.000000000000000000, -0.000000000000000000 ) ) ;
#456=ADVANCED_FACE ( 'NONE', ( #3832 ), #10195, .T. ) ;
#460=VECTOR ( 'NONE', #7441, 1000.000000000000000 ) ;
#470=CYLINDRICAL_SURFACE ( 'NONE', #5849, 84.99999999999997158 ) ;
#472=CIRCLE ( 'NONE', #7564, 4.695405383896011919 ) ;
#479=ORIENTED_EDGE ( 'NONE', *, *, #12252, .F. ) ;
#486=CARTESIAN_POINT ( 'NONE',  ( 54.99999999999999289, 515.4878487013597805, -546.7230258972048205 ) ) ;
#490=LINE ( 'NONE', #9679, #7358 ) ;
#493=CARTESIAN_POINT ( 'NONE',  ( 55.99999999999989342, 549.5810598491746077, -518.1154249974242703 ) ) ;
#502=CARTESIAN_POINT ( 'NONE',  ( -55.99999999999989342, 473.6663340069158039, -561.9448123979092315 ) ) ;
#507=CIRCLE ( 'NONE', #10098, 9.000000000000007105 ) ;
#524=CARTESIAN_POINT ( 'NONE',  ( 55.99999999999989342, 549.5810598491749488, -575.3306267969850296 ) ) ;
#533=CARTESIAN_POINT ( 'NONE',  ( 49.99999999999999289, 515.4878487013597805, -461.7230258972048205 ) ) ;
#537=CIRCLE ( 'NONE', #16696, 4.695405383896011919 ) ;
#544=VERTEX_POINT ( 'NONE', #15850 ) ;
#546=CARTESIAN_POINT ( 'NONE',  ( 46.99999999999988631, 549.5810598491749488, -580.0260321808809749 ) ) ;
#550=ORIENTED_EDGE ( 'NONE', *, *, #4758, .F. ) ;
#553=EDGE_CURVE ( 'NONE', #8853, #13498, #14617, .T. ) ;
#563=CARTESIAN_POINT ( 'NONE',  ( 45.00000000000000000, 473.6663340069157471, -531.5012393965008641 ) ) ;
#565=CARTESIAN_POINT ( 'NONE',  ( 54.99999999999999289, 334.9272574771864015, -321.9943432880672276 ) ) ;
#567=PLANE ( 'NONE',  #12865 ) ;
#568=CARTESIAN_POINT ( 'NONE',  ( -45.00000000000000000, 493.2350855268086320, -508.1801094700848580 ) ) ;
#569=DIRECTION ( 'NONE',  ( 1.000000000000000000, 0.000000000000000000, 0.000000000000000000 ) ) ;
#575=ORIENTED_EDGE ( 'NONE', *, *, #10890, .F. ) ;
#576=ORIENTED_EDGE ( 'NONE', *, *, #14354, .T. ) ;
#581=DIRECTION ( 'NONE',  ( -1.000000000000000000, -0.000000000000000000, -0.000000000000000000 ) ) ;
#588=DIRECTION ( 'NONE',  ( 0.000000000000000000, 0.000000000000000000, -1.000000000000000000 ) ) ;
#599=LINE ( 'NONE', #3258, #12217 ) ;
#601=DIRECTION ( 'NONE',  ( 1.000000000000000000, -0.000000000000000000, -0.000000000000000000 ) ) ;
#608=DIRECTION ( 'NONE',  ( 1.000000000000000000, -0.000000000000000000, -0.000000000000000000 ) ) ;
#614=VERTEX_POINT ( 'NONE', #13461 ) ;
#617=DIRECTION ( 'NONE',  ( -1.000000000000000000, -0.000000000000000000, -0.000000000000000000 ) ) ;
#618=ADVANCED_FACE ( 'NONE', ( #15247 ), #15699, .T. ) ;
#631=AXIS2_PLACEMENT_3D ( 'NONE', #2906, #4290, #4103 ) ;
#632=DIRECTION ( 'NONE',  ( 1.000000000000000000, -0.000000000000000000, 0.000000000000000000 ) ) ;
#644=FACE_OUTER_BOUND ( 'NONE', #16902, .T. ) ;
#649=DIRECTION ( 'NONE',  ( 0.000000000000000000, 0.000000000000000000, -1.000000000000000000 ) ) ;
#653=AXIS2_PLACEMENT_3D ( 'NONE', #5751, #11950, #5409 ) ;
#654=FACE_OUTER_BOUND ( 'NONE', #3552, .T. ) ;
#656=EDGE_LOOP ( 'NONE', ( #8777, #14028, #11460, #5148 ) ) ;
#662=ORIENTED_EDGE ( 'NONE', *, *, #3733, .T. ) ;
#663=EDGE_CURVE ( 'NONE', #3748, #11164, #8302, .T. ) ;
#680=CARTESIAN_POINT ( 'NONE',  ( -54.99999999999999289, 515.4878487013597805, -546.7230258972048205 ) ) ;
#681=DIRECTION ( 'NONE',  ( -1.000000000000000000, -0.000000000000000000, -0.000000000000000000 ) ) ;
#691=AXIS2_PLACEMENT_3D ( 'NONE', #9355, #14691, #13486 ) ;
#697=CARTESIAN_POINT ( 'NONE',  ( 49.99999999999999289, 515.4878487013597805, -546.7230258972048205 ) ) ;
#699=CARTESIAN_POINT ( 'NONE',  ( 45.00000000000000000, 523.2161522479893847, -604.2478186815853860 ) ) ;
#713=DIRECTION ( 'NONE',  ( 1.000000000000000000, 0.000000000000000000, 0.000000000000000000 ) ) ;
#720=ADVANCED_FACE ( 'NONE', ( #2013 ), #3235, .T. ) ;
#738=TOROIDAL_SURFACE ( 'NONE', #7030, 4.695405383895982609, 9.000000000000000000 ) ;
#739=DIRECTION ( 'NONE',  ( 1.000000000000000000, 0.000000000000000000, 0.000000000000000000 ) ) ;
#741=FACE_BOUND ( 'NONE', #3110, .T. ) ;
#744=CARTESIAN_POINT ( 'NONE',  ( 46.99999999999988631, 559.9933750504617365, -546.7230258972048205 ) ) ;
#748=VERTEX_POINT ( 'NONE', #2182 ) ;
#750=VERTEX_POINT ( 'NONE', #11127 ) ;
#752=AXIS2_PLACEMENT_3D ( 'NONE', #10958, #569, #11207 ) ;
#759=CARTESIAN_POINT ( 'NONE',  ( 44.99999999999998579, 515.4878487013597805, -571.7230258972048205 ) ) ;
#760=DIRECTION ( 'NONE',  ( 1.000000000000000000, -0.000000000000000000, 0.000000000000000000 ) ) ;
#761=ORIENTED_EDGE ( 'NONE', *, *, #4663, .F. ) ;
#762=CARTESIAN_POINT ( 'NONE',  ( 46.99999999999988631, 473.6663340069157471, -531.5012393965008641 ) ) ;
#765=CIRCLE ( 'NONE', #3503, 25.00000000000002132 ) ;
#769=DIRECTION ( 'NONE',  ( 0.000000000000000000, 0.000000000000000000, 1.000000000000000000 ) ) ;
#773=DIRECTION ( 'NONE',  ( -1.000000000000000000, 0.000000000000000000, -0.000000000000000000 ) ) ;
#781=ORIENTED_EDGE ( 'NONE', *, *, #4458, .T. ) ;
#786=EDGE_CURVE ( 'NONE', #9290, #5350, #6103, .T. ) ;
#794=LINE ( 'NONE', #871, #6349 ) ;
#802=DIRECTION ( 'NONE',  ( -1.000000000000000000, -0.000000000000000000, -0.000000000000000000 ) ) ;
#818=LINE ( 'NONE', #565, #9425 ) ;
#836=LINE ( 'NONE', #13972, #7247 ) ;
#838=CARTESIAN_POINT ( 'NONE',  ( 55.99999999999989342, 473.6663340069158039, -557.2494070140132862 ) ) ;
#848=DIRECTION ( 'NONE',  ( -1.000000000000000000, -0.000000000000000000, -0.000000000000000000 ) ) ;
#852=DIRECTION ( 'NONE',  ( 0.000000000000000000, 0.000000000000000000, 1.000000000000000000 ) ) ;
#855=DIRECTION ( 'NONE',  ( 1.000000000000000000, 0.000000000000000000, 0.000000000000000000 ) ) ;
#858=DIRECTION ( 'NONE',  ( 0.000000000000000000, 0.000000000000000000, -1.000000000000000000 ) ) ;
#871=CARTESIAN_POINT ( 'NONE',  ( 54.99999999999999289, 515.4878487013597805, -461.7230258972048205 ) ) ;
#873=EDGE_LOOP ( 'NONE', ( #5889, #10233 ) ) ;
#881=ORIENTED_EDGE ( 'NONE', *, *, #16843, .T. ) ;
#885=AXIS2_PLACEMENT_3D ( 'NONE', #15348, #2118, #15017 ) ;
#888=ORIENTED_EDGE ( 'NONE', *, *, #8243, .T. ) ;
#904=DIRECTION ( 'NONE',  ( 0.000000000000000000, 0.000000000000000000, -1.000000000000000000 ) ) ;
#907=ORIENTED_EDGE ( 'NONE', *, *, #3318, .F. ) ;
#912=TOROIDAL_SURFACE ( 'NONE', #10781, 4.695405383895982609, 9.000000000000000000 ) ;
#921=CARTESIAN_POINT ( 'NONE',  ( 54.99999999999999289, 459.5014304922595443, -192.4166442068759579 ) ) ;
#928=DIRECTION ( 'NONE',  ( 0.000000000000000000, -1.000000000000000000, 0.000000000000000000 ) ) ;
#943=CARTESIAN_POINT ( 'NONE',  ( 45.00000000000000000, 493.2350855268092573, -598.9613477082210693 ) ) ;
#945=FACE_OUTER_BOUND ( 'NONE', #12335, .T. ) ;
#947=ORIENTED_EDGE ( 'NONE', *, *, #7819, .F. ) ;
#948=DIRECTION ( 'NONE',  ( -1.000000000000000000, 0.000000000000000000, 0.000000000000000000 ) ) ;
#957=EDGE_CURVE ( 'NONE', #5265, #14388, #10680, .T. ) ;
#958=DIRECTION ( 'NONE',  ( 1.000000000000000000, 0.000000000000000000, 0.000000000000000000 ) ) ;
#959=ORIENTED_EDGE ( 'NONE', *, *, #10890, .T. ) ;
#963=VERTEX_POINT ( 'NONE', #8006 ) ;
#966=ORIENTED_EDGE ( 'NONE', *, *, #15704, .T. ) ;
#982=DIRECTION ( 'NONE',  ( 0.000000000000000000, -0.9848077530122086864, 0.1736481776669273613 ) ) ;
#984=FACE_BOUND ( 'NONE', #6638, .T. ) ;
#988=EDGE_LOOP ( 'NONE', ( #15839, #11298, #10408, #266 ) ) ;
#990=ADVANCED_FACE ( 'NONE', ( #10855 ), #912, .T. ) ;
#993=CARTESIAN_POINT ( 'NONE',  ( -55.99999999999988631, 0.000000000000000000, 0.000000000000000000 ) ) ;
#996=CARTESIAN_POINT ( 'NONE',  ( 46.99999999999988631, 473.6663340069157471, -545.1966447803968094 ) ) ;
#1000=EDGE_CURVE ( 'NONE', #13474, #21, #3113, .T. ) ;
#1008=ORIENTED_EDGE ( 'NONE', *, *, #4654, .T. ) ;
#1014=CARTESIAN_POINT ( 'NONE',  ( 46.99999999999988631, 523.2161522479893847, -590.5524132976893270 ) ) ;
#1015=ORIENTED_EDGE ( 'NONE', *, *, #13635, .F. ) ;
#1016=AXIS2_PLACEMENT_3D ( 'NONE', #3650, #15408, #904 ) ;
#1018=TOROIDAL_SURFACE ( 'NONE', #16362, 4.695405383895982609, 9.000000000000000000 ) ;
#1022=FACE_OUTER_BOUND ( 'NONE', #2431, .T. ) ;
#1037=FACE_OUTER_BOUND ( 'NONE', #656, .T. ) ;
#1038=AXIS2_PLACEMENT_3D ( 'NONE', #4074, #10596, #10679 ) ;
#1041=DIRECTION ( 'NONE',  ( 1.000000000000000000, -0.000000000000000000, -0.000000000000000000 ) ) ;
#1043=CARTESIAN_POINT ( 'NONE',  ( 46.99999999999988631, 549.5810598491749488, -575.3306267969850296 ) ) ;
#1044=VERTEX_POINT ( 'NONE', #13614 ) ;
#1045=DIRECTION ( 'NONE',  ( -1.000000000000000000, -0.000000000000000000, 0.000000000000000000 ) ) ;
#1048=CIRCLE ( 'NONE', #7066, 13.69540538389598083 ) ;
#1050=ORIENTED_EDGE ( 'NONE', *, *, #7090, .T. ) ;
#1053=ORIENTED_EDGE ( 'NONE', *, *, #15007, .T. ) ;
#1059=DIRECTION ( 'NONE',  ( 0.000000000000000000, 0.000000000000000000, 1.000000000000000000 ) ) ;
#1061=DIRECTION ( 'NONE',  ( -1.000000000000000000, 0.000000000000000000, 0.000000000000000000 ) ) ;
#1073=VERTEX_POINT ( 'NONE', #15296 ) ;
#1088=CARTESIAN_POINT ( 'NONE',  ( 46.99999999999988631, 549.5810598491746077, -531.8108303813202156 ) ) ;
#1095=EDGE_LOOP ( 'NONE', ( #12425, #5383 ) ) ;
#1099=DIRECTION ( 'NONE',  ( -1.000000000000000000, 0.000000000000000000, 0.000000000000000000 ) ) ;
#1103=CARTESIAN_POINT ( 'NONE',  ( -45.00000000000000000, 515.4878487013597805, -546.7230258972048205 ) ) ;
#1125=ADVANCED_FACE ( 'NONE', ( #16655 ), #470, .F. ) ;
#1139=AXIS2_PLACEMENT_3D ( 'NONE', #14241, #6310, #11563 ) ;
#1140=CARTESIAN_POINT ( 'NONE',  ( -46.99999999999988631, 549.5810598491746077, -518.1154249974242703 ) ) ;
#1151=AXIS2_PLACEMENT_3D ( 'NONE', #11728, #1512, #13284 ) ;
#1154=DIRECTION ( 'NONE',  ( 0.000000000000000000, 0.000000000000000000, -1.000000000000000000 ) ) ;
#1171=AXIS2_PLACEMENT_3D ( 'NONE', #9262, #7871, #12008 ) ;
#1186=AXIS2_PLACEMENT_3D ( 'NONE', #8388, #1774, #230 ) ;
#1188=VERTEX_POINT ( 'NONE', #12959 ) ;
#1196=VERTEX_POINT ( 'NONE', #14423 ) ;
#1198=DIRECTION ( 'NONE',  ( -1.000000000000000000, -0.000000000000000000, 0.000000000000000000 ) ) ;
#1199=EDGE_CURVE ( 'NONE', #13085, #5980, #15985, .T. ) ;
#1208=EDGE_CURVE ( 'NONE', #9380, #4994, #11562, .T. ) ;
#1210=CARTESIAN_POINT ( 'NONE',  ( 45.00000000000000000, 515.4878487013597805, -486.7230258972047636 ) ) ;
#1214=ORIENTED_EDGE ( 'NONE', *, *, #5476, .T. ) ;
#1215=CARTESIAN_POINT ( 'NONE',  ( -45.00000000000000000, 493.2350855268086320, -508.1801094700848580 ) ) ;
#1228=EDGE_CURVE ( 'NONE', #11320, #13664, #3899, .T. ) ;
#1232=CYLINDRICAL_SURFACE ( 'NONE', #4228, 59.99999999999994316 ) ;
#1234=VECTOR ( 'NONE', #7686, 1000.000000000000000 ) ;
#1241=EDGE_LOOP ( 'NONE', ( #12752, #12919, #4251, #4555 ) ) ;
#1243=ORIENTED_EDGE ( 'NONE', *, *, #286, .T. ) ;
#1244=DIRECTION ( 'NONE',  ( 1.000000000000000000, -0.000000000000000000, -0.000000000000000000 ) ) ;
#1268=AXIS2_PLACEMENT_3D ( 'NONE', #10126, #1099, #2388 ) ;
#1276=LINE ( 'NONE', #14662, #2418 ) ;
#1277=DIRECTION ( 'NONE',  ( 1.000000000000000000, 0.000000000000000000, 0.000000000000000000 ) ) ;
#1280=CIRCLE ( 'NONE', #2647, 4.695405383896011919 ) ;
#1286=DIRECTION ( 'NONE',  ( 0.000000000000000000, 0.000000000000000000, -1.000000000000000000 ) ) ;
#1292=EDGE_CURVE ( 'NONE', #13450, #1044, #16815, .T. ) ;
#1303=ORIENTED_EDGE ( 'NONE', *, *, #13173, .F. ) ;
#1312=DIRECTION ( 'NONE',  ( -1.000000000000000000, -0.000000000000000000, -0.000000000000000000 ) ) ;
#1316=CARTESIAN_POINT ( 'NONE',  ( 44.99999999999998579, 515.4878487013597805, -521.7230258972047068 ) ) ;
#1319=DIRECTION ( 'NONE',  ( 1.000000000000000000, 0.000000000000000000, -0.000000000000000000 ) ) ;
#1322=EDGE_CURVE ( 'NONE', #15297, #13085, #2233, .T. ) ;
#1327=DIRECTION ( 'NONE',  ( 0.000000000000000000, 0.000000000000000000, 1.000000000000000000 ) ) ;
#1328=AXIS2_PLACEMENT_3D ( 'NONE', #1103, #11574, #14250 ) ;
#1331=ORIENTED_EDGE ( 'NONE', *, *, #8487, .T. ) ;
#1332=LINE ( 'NONE', #308, #13515 ) ;
#1340=FACE_BOUND ( 'NONE', #1383, .T. ) ;
#1344=DIRECTION ( 'NONE',  ( 0.000000000000000000, 0.000000000000000000, -1.000000000000000000 ) ) ;
#1358=DIRECTION ( 'NONE',  ( 0.000000000000000000, 0.000000000000000000, -1.000000000000000000 ) ) ;
#1366=PLANE ( 'NONE',  #691 ) ;
#1369=CIRCLE ( 'NONE', #15902, 13.69540538389598083 ) ;
#1372=DIRECTION ( 'NONE',  ( 0.000000000000000000, 0.9848077530122062440, 0.1736481776669404620 ) ) ;
#1375=VERTEX_POINT ( 'NONE', #6843 ) ;
#1382=ORIENTED_EDGE ( 'NONE', *, *, #11302, .F. ) ;
#1383=EDGE_LOOP ( 'NONE', ( #947, #1303 ) ) ;
#1384=DIRECTION ( 'NONE',  ( 1.000000000000000000, 0.000000000000000000, 0.000000000000000000 ) ) ;
#1386=VERTEX_POINT ( 'NONE', #339 ) ;
#1392=DIRECTION ( 'NONE',  ( -1.000000000000000000, 0.000000000000000000, -0.000000000000000000 ) ) ;
#1395=EDGE_CURVE ( 'NONE', #5700, #15832, #15760, .T. ) ;
#1399=ORIENTED_EDGE ( 'NONE', *, *, #15739, .F. ) ;
#1401=EDGE_LOOP ( 'NONE', ( #12221, #4419, #11440, #8754 ) ) ;
#1404=ORIENTED_EDGE ( 'NONE', *, *, #8025, .T. ) ;
#1409=ADVANCED_FACE ( 'NONE', ( #50 ), #4007, .T. ) ;
#1421=CARTESIAN_POINT ( 'NONE',  ( -55.99999999999989342, 549.5810598491746077, -518.1154249974242703 ) ) ;
#1432=CARTESIAN_POINT ( 'NONE',  ( 55.99999999999989342, 523.2161522479888163, -502.8936384967199729 ) ) ;
#1437=EDGE_CURVE ( 'NONE', #6153, #3748, #10694, .T. ) ;
#1443=CIRCLE ( 'NONE', #3374, 4.695405383896011919 ) ;
#1444=FACE_OUTER_BOUND ( 'NONE', #15279, .T. ) ;
#1447=LINE ( 'NONE', #7018, #6190 ) ;
#1455=FACE_OUTER_BOUND ( 'NONE', #11040, .T. ) ;
#1460=AXIS2_PLACEMENT_3D ( 'NONE', #15518, #13026, #11469 ) ;
#1464=CARTESIAN_POINT ( 'NONE',  ( -55.99999999999989342, 473.6663340069157471, -536.1966447803968094 ) ) ;
#1475=CARTESIAN_POINT ( 'NONE',  ( 55.99999999999989342, 473.6663340069158039, -575.6402177818052905 ) ) ;
#1476=CIRCLE ( 'NONE', #6943, 187.4999999999998863 ) ;
#1480=AXIS2_PLACEMENT_3D ( 'NONE', #235, #6477, #4179 ) ;
#1481=VERTEX_POINT ( 'NONE', #11992 ) ;
#1483=EDGE_CURVE ( 'NONE', #15480, #13498, #15846, .T. ) ;
#1484=EDGE_LOOP ( 'NONE', ( #575, #11394 ) ) ;
#1488=AXIS2_PLACEMENT_3D ( 'NONE', #3280, #8693, #15217 ) ;
#1489=ORIENTED_EDGE ( 'NONE', *, *, #11917, .F. ) ;
#1500=DIRECTION ( 'NONE',  ( 0.000000000000000000, 0.000000000000000000, 1.000000000000000000 ) ) ;
#1505=AXIS2_PLACEMENT_3D ( 'NONE', #1421, #7596, #8993 ) ;
#1512=DIRECTION ( 'NONE',  ( -1.000000000000000000, -0.000000000000000000, -0.000000000000000000 ) ) ;
#1517=DIRECTION ( 'NONE',  ( -1.000000000000000000, -0.000000000000000000, -0.000000000000000000 ) ) ;
#1520=DIRECTION ( 'NONE',  ( 0.000000000000000000, 0.000000000000000000, -1.000000000000000000 ) ) ;
#1540=CARTESIAN_POINT ( 'NONE',  ( -46.99999999999988631, 493.2350855268086320, -508.1801094700848580 ) ) ;
#1542=VERTEX_POINT ( 'NONE', #8386 ) ;
#1545=AXIS2_PLACEMENT_3D ( 'NONE', #6781, #14701, #6859 ) ;
#1552=DIRECTION ( 'NONE',  ( 0.000000000000000000, -1.000000000000000000, 0.000000000000000000 ) ) ;
#1555=DIRECTION ( 'NONE',  ( 0.000000000000000000, 0.000000000000000000, 1.000000000000000000 ) ) ;
#1558=DIRECTION ( 'NONE',  ( 1.000000000000000000, -0.000000000000000000, -0.000000000000000000 ) ) ;
#1562=CARTESIAN_POINT ( 'NONE',  ( 55.99999999999989342, 549.5810598491749488, -575.3306267969850296 ) ) ;
#1565=LINE ( 'NONE', #1475, #11918 ) ;
#1577=ADVANCED_FACE ( 'NONE', ( #10872 ), #6992, .T. ) ;
#1594=DIRECTION ( 'NONE',  ( 0.000000000000000000, 1.000000000000000000, 1.224646799147353207E-16 ) ) ;
#1596=DIRECTION ( 'NONE',  ( 0.000000000000000000, -0.3420201433256630508, -0.9396926207859104263 ) ) ;
#1602=CYLINDRICAL_SURFACE ( 'NONE', #1480, 13.69540538389596485 ) ;
#1609=ADVANCED_FACE ( 'NONE', ( #644 ), #14742, .T. ) ;
#1618=DIRECTION ( 'NONE',  ( 1.000000000000000000, 0.000000000000000000, 0.000000000000000000 ) ) ;
#1621=DIRECTION ( 'NONE',  ( 0.000000000000000000, 1.000000000000000000, 1.224646799147353207E-16 ) ) ;
#1628=CIRCLE ( 'NONE', #14257, 84.99999999999997158 ) ;
#1631=EDGE_CURVE ( 'NONE', #16404, #4508, #9674, .T. ) ;
#1632=DIRECTION ( 'NONE',  ( 0.000000000000000000, 0.000000000000000000, -1.000000000000000000 ) ) ;
#1638=ADVANCED_FACE ( 'NONE', ( #12325 ), #13674, .T. ) ;
#1650=ORIENTED_EDGE ( 'NONE', *, *, #9582, .T. ) ;
#1653=CARTESIAN_POINT ( 'NONE',  ( -54.99999999999999289, 658.4713480608917280, -425.4301204538002139 ) ) ;
#1656=ORIENTED_EDGE ( 'NONE', *, *, #1437, .T. ) ;
#1658=CYLINDRICAL_SURFACE ( 'NONE', #12715, 13.69540538389601991 ) ;
#1666=ORIENTED_EDGE ( 'NONE', *, *, #14517, .F. ) ;
#1667=DIRECTION ( 'NONE',  ( 0.000000000000000000, 0.000000000000000000, 1.000000000000000000 ) ) ;
#1673=CIRCLE ( 'NONE', #3049, 13.69540538389601991 ) ;
#1680=CARTESIAN_POINT ( 'NONE',  ( 54.99999999999999289, 173.0499717945046996, 146.7982946275220968 ) ) ;
#1690=CARTESIAN_POINT ( 'NONE',  ( -45.00000000000000000, 523.2161522479893847, -604.2478186815853860 ) ) ;
#1696=CARTESIAN_POINT ( 'NONE',  ( 46.99999999999988631, 493.2350855268092573, -598.9613477082210693 ) ) ;
#1710=EDGE_CURVE ( 'NONE', #963, #13664, #5708, .T. ) ;
#1718=DIRECTION ( 'NONE',  ( 0.000000000000000000, 0.000000000000000000, 1.000000000000000000 ) ) ;
#1722=TOROIDAL_SURFACE ( 'NONE', #15152, 4.695405383895982609, 9.000000000000000000 ) ;
#1739=VECTOR ( 'NONE', #2775, 1000.000000000000000 ) ;
#1740=AXIS2_PLACEMENT_3D ( 'NONE', #4442, #15942, #16125 ) ;
#1753=DIRECTION ( 'NONE',  ( -1.000000000000000000, -0.000000000000000000, 0.000000000000000000 ) ) ;
#1771=FACE_OUTER_BOUND ( 'NONE', #16670, .T. ) ;
#1774=DIRECTION ( 'NONE',  ( -1.000000000000000000, 0.000000000000000000, -0.000000000000000000 ) ) ;
#1786=AXIS2_PLACEMENT_3D ( 'NONE', #14256, #1198, #6328 ) ;
#1793=ORIENTED_EDGE ( 'NONE', *, *, #9295, .T. ) ;
#1797=DIRECTION ( 'NONE',  ( 0.000000000000000000, 0.000000000000000000, -1.000000000000000000 ) ) ;
#1800=DIRECTION ( 'NONE',  ( -1.000000000000000000, -0.000000000000000000, 0.000000000000000000 ) ) ;
#1803=DIRECTION ( 'NONE',  ( 0.000000000000000000, 0.000000000000000000, -1.000000000000000000 ) ) ;
#1804=CARTESIAN_POINT ( 'NONE',  ( -55.99999999999989342, 493.2350855268092573, -580.5705369404290650 ) ) ;
#1806=CARTESIAN_POINT ( 'NONE',  ( 46.99999999999988631, 493.2350855268092573, -589.9613477082210693 ) ) ;
#1817=EDGE_CURVE ( 'NONE', #6348, #3860, #1048, .T. ) ;
#1819=CIRCLE ( 'NONE', #7275, 9.000000000000007105 ) ;
#1826=CARTESIAN_POINT ( 'NONE',  ( -49.99999999999999289, 515.4878487013597805, -606.7230258972047068 ) ) ;
#1827=AXIS2_PLACEMENT_3D ( 'NONE', #15975, #13497, #14954 ) ;
#1830=VECTOR ( 'NONE', #16891, 1000.000000000000000 ) ;
#1842=EDGE_LOOP ( 'NONE', ( #8254, #8543, #10834, #15114 ) ) ;
#1849=DIRECTION ( 'NONE',  ( 0.000000000000000000, -0.8660254037844363761, -0.5000000000000039968 ) ) ;
#1855=EDGE_CURVE ( 'NONE', #14215, #544, #2145, .T. ) ;
#1857=CARTESIAN_POINT ( 'NONE',  ( 55.99999999999989342, 549.5810598491746077, -518.1154249974242703 ) ) ;
#1860=DIRECTION ( 'NONE',  ( 1.000000000000000000, 0.000000000000000000, 0.000000000000000000 ) ) ;
#1868=CARTESIAN_POINT ( 'NONE',  ( 46.99999999999988631, 523.2161522479893847, -595.2478186815853860 ) ) ;
#1869=DIRECTION ( 'NONE',  ( -1.000000000000000000, 0.000000000000000000, -0.000000000000000000 ) ) ;
#1871=DIRECTION ( 'NONE',  ( 1.000000000000000000, 0.000000000000000000, 0.000000000000000000 ) ) ;
#1874=ADVANCED_FACE ( 'NONE', ( #13238, #5583 ), #14700, .F. ) ;
#1878=CARTESIAN_POINT ( 'NONE',  ( 55.99999999999989342, 493.2350855268086320, -508.1801094700848580 ) ) ;
#1882=CIRCLE ( 'NONE', #11473, 59.99999999999994316 ) ;
#1883=SHAPE_REPRESENTATION ( 'Part6', ( #1488 ), #16030 ) ;
#1892=ORIENTED_EDGE ( 'NONE', *, *, #1395, .T. ) ;
#1914=( NAMED_UNIT ( * ) SI_UNIT ( $, .STERADIAN. ) SOLID_ANGLE_UNIT ( ) );
#1923=CARTESIAN_POINT ( 'NONE',  ( 46.99999999999988631, 493.2350855268086320, -508.1801094700848580 ) ) ;
#1926=DIRECTION ( 'NONE',  ( 0.000000000000000000, 0.000000000000000000, -1.000000000000000000 ) ) ;
#1928=ORIENTED_EDGE ( 'NONE', *, *, #12665, .F. ) ;
#1931=CIRCLE ( 'NONE', #7397, 13.69540538389601991 ) ;
#1946=VERTEX_POINT ( 'NONE', #12209 ) ;
#1955=AXIS2_PLACEMENT_3D ( 'NONE', #7847, #15843, #13107 ) ;
#1959=DIRECTION ( 'NONE',  ( 0.000000000000000000, 0.000000000000000000, 1.000000000000000000 ) ) ;
#1961=VECTOR ( 'NONE', #13730, 1000.000000000000000 ) ;
#1963=CARTESIAN_POINT ( 'NONE',  ( -46.99999999999988631, 473.6663340069158039, -561.9448123979092315 ) ) ;
#1985=CARTESIAN_POINT ( 'NONE',  ( -55.99999999999989342, 473.6663340069158039, -561.9448123979092315 ) ) ;
#1987=EDGE_LOOP ( 'NONE', ( #15123, #3976, #13341, #8270 ) ) ;
#1995=VERTEX_POINT ( 'NONE', #8679 ) ;
#2007=AXIS2_PLACEMENT_3D ( 'NONE', #15258, #12676, #6137 ) ;
#2013=FACE_OUTER_BOUND ( 'NONE', #11234, .T. ) ;
#2014=CIRCLE ( 'NONE', #11610, 13.69540538389601991 ) ;
#2024=AXIS2_PLACEMENT_3D ( 'NONE', #4522, #3238, #11129 ) ;
#2028=EDGE_CURVE ( 'NONE', #10388, #1481, #8195, .T. ) ;
#2031=DIRECTION ( 'NONE',  ( -1.000000000000000000, 0.000000000000000000, 0.000000000000000000 ) ) ;
#2041=ORIENTED_EDGE ( 'NONE', *, *, #6763, .T. ) ;
#2047=FILL_AREA_STYLE_COLOUR ( '', #7195 ) ;
#2050=CIRCLE ( 'NONE', #12761, 4.695405383895955964 ) ;
#2053=CARTESIAN_POINT ( 'NONE',  ( -45.00000000000000000, 559.9933750504617365, -546.7230258972048205 ) ) ;
#2066=ORIENTED_EDGE ( 'NONE', *, *, #10313, .F. ) ;
#2079=EDGE_LOOP ( 'NONE', ( #12382, #14204, #2230, #959 ) ) ;
#2081=PLANE ( 'NONE',  #8050 ) ;
#2085=CIRCLE ( 'NONE', #8683, 13.69540538389601991 ) ;
#2097=CARTESIAN_POINT ( 'NONE',  ( 55.99999999999989342, 523.2161522479893847, -590.5524132976893270 ) ) ;
#2100=ORIENTED_EDGE ( 'NONE', *, *, #6851, .F. ) ;
#2115=ORIENTED_EDGE ( 'NONE', *, *, #9611, .F. ) ;
#2118=DIRECTION ( 'NONE',  ( 0.000000000000000000, -1.000000000000000000, 0.000000000000000000 ) ) ;
#2121=CARTESIAN_POINT ( 'NONE',  ( 55.99999999999989342, 523.2161522479893847, -590.5524132976893270 ) ) ;
#2123=DIRECTION ( 'NONE',  ( -1.000000000000000000, -0.000000000000000000, -0.000000000000000000 ) ) ;
#2126=DIRECTION ( 'NONE',  ( -1.000000000000000000, 0.000000000000000000, 0.000000000000000000 ) ) ;
#2129=VECTOR ( 'NONE', #7523, 1000.000000000000000 ) ;
#2131=ORIENTED_EDGE ( 'NONE', *, *, #15166, .T. ) ;
#2136=CARTESIAN_POINT ( 'NONE',  ( -55.99999999999989342, 473.6663340069158039, -561.9448123979092315 ) ) ;
#2137=LINE ( 'NONE', #12616, #11139 ) ;
#2138=ORIENTED_EDGE ( 'NONE', *, *, #5649, .T. ) ;
#2145=CIRCLE ( 'NONE', #2409, 13.69540538389601991 ) ;
#2157=CARTESIAN_POINT ( 'NONE',  ( 55.99999999999989342, 493.2350855268086320, -508.1801094700848580 ) ) ;
#2166=ORIENTED_EDGE ( 'NONE', *, *, #8686, .F. ) ;
#2168=ADVANCED_FACE ( 'NONE', ( #9014 ), #16569, .T. ) ;
#2169=ORIENTED_EDGE ( 'NONE', *, *, #11404, .T. ) ;
#2171=ADVANCED_FACE ( 'NONE', ( #12707, #945 ), #6165, .F. ) ;
#2178=CARTESIAN_POINT ( 'NONE',  ( 55.99999999999989342, 549.5810598491749488, -575.3306267969850296 ) ) ;
#2179=FACE_BOUND ( 'NONE', #1095, .T. ) ;
#2180=ORIENTED_EDGE ( 'NONE', *, *, #15459, .F. ) ;
#2182=CARTESIAN_POINT ( 'NONE',  ( -45.00000000000000000, 559.9933750504617365, -533.0276205133087615 ) ) ;
#2184=DIRECTION ( 'NONE',  ( 1.000000000000000000, 0.000000000000000000, 0.000000000000000000 ) ) ;
#2188=DIRECTION ( 'NONE',  ( 1.000000000000000000, -0.000000000000000000, 0.000000000000000000 ) ) ;
#2189=AXIS2_PLACEMENT_3D ( 'NONE', #9421, #14751, #13550 ) ;
#2192=DIRECTION ( 'NONE',  ( 0.000000000000000000, 0.000000000000000000, -1.000000000000000000 ) ) ;
#2194=DIRECTION ( 'NONE',  ( 0.000000000000000000, 0.000000000000000000, 1.000000000000000000 ) ) ;
#2195=ORIENTED_EDGE ( 'NONE', *, *, #7824, .F. ) ;
#2197=CIRCLE ( 'NONE', #9618, 13.69540538389601991 ) ;
#2198=CYLINDRICAL_SURFACE ( 'NONE', #12808, 60.00000000000000000 ) ;
#2222=DIRECTION ( 'NONE',  ( 0.000000000000000000, 0.000000000000000000, 1.000000000000000000 ) ) ;
#2228=FACE_OUTER_BOUND ( 'NONE', #10422, .T. ) ;
#2229=AXIS2_PLACEMENT_3D ( 'NONE', #14202, #13086, #3985 ) ;
#2230=ORIENTED_EDGE ( 'NONE', *, *, #7181, .T. ) ;
#2231=DIRECTION ( 'NONE',  ( 0.000000000000000000, 0.000000000000000000, -1.000000000000000000 ) ) ;
#2233=CIRCLE ( 'NONE', #12940, 13.69540538389596485 ) ;
#2234=EDGE_CURVE ( 'NONE', #12483, #4508, #16959, .T. ) ;
#2242=EDGE_CURVE ( 'NONE', #9686, #1196, #490, .T. ) ;
#2243=VERTEX_POINT ( 'NONE', #16280 ) ;
#2250=VERTEX_POINT ( 'NONE', #4431 ) ;
#2254=EDGE_CURVE ( 'NONE', #11097, #1073, #9022, .T. ) ;
#2258=CARTESIAN_POINT ( 'NONE',  ( 55.99999999999989342, 493.2350855268092573, -580.5705369404290650 ) ) ;
#2260=FACE_OUTER_BOUND ( 'NONE', #13023, .T. ) ;
#2261=CIRCLE ( 'NONE', #8580, 4.695405383896011919 ) ;
#2268=EDGE_CURVE ( 'NONE', #11320, #7813, #1276, .T. ) ;
#2279=CARTESIAN_POINT ( 'NONE',  ( 45.00000000000000000, 515.4878487013597805, -486.7230258972047636 ) ) ;
#2280=ORIENTED_EDGE ( 'NONE', *, *, #10841, .T. ) ;
#2281=UNCERTAINTY_MEASURE_WITH_UNIT (LENGTH_MEASURE( 1.000000000000000082E-05 ), #3261, 'distance_accuracy_value', 'NONE');
#2284=CARTESIAN_POINT ( 'NONE',  ( -45.00000000000000000, 515.4878487013597805, -546.7230258972048205 ) ) ;
#2292=CARTESIAN_POINT ( 'NONE',  ( 55.99999999999989342, 559.9933750504617365, -551.4184312811007658 ) ) ;
#2293=CYLINDRICAL_SURFACE ( 'NONE', #12560, 13.69540538389601991 ) ;
#2298=CIRCLE ( 'NONE', #16029, 4.695405383896011919 ) ;
#2299=ORIENTED_EDGE ( 'NONE', *, *, #4684, .T. ) ;
#2304=DIRECTION ( 'NONE',  ( -1.000000000000000000, 0.000000000000000000, -0.000000000000000000 ) ) ;
#2309=DIRECTION ( 'NONE',  ( 1.000000000000000000, -0.000000000000000000, -0.000000000000000000 ) ) ;
#2311=EDGE_CURVE ( 'NONE', #5700, #13853, #2884, .T. ) ;
#2335=EDGE_CURVE ( 'NONE', #9156, #15233, #1882, .T. ) ;
#2344=FACE_OUTER_BOUND ( 'NONE', #873, .T. ) ;
#2348=FACE_OUTER_BOUND ( 'NONE', #7908, .T. ) ;
#2352=AXIS2_PLACEMENT_3D ( 'NONE', #11797, #40, #2779 ) ;
#2367=EDGE_CURVE ( 'NONE', #3583, #1386, #6527, .T. ) ;
#2368=DIRECTION ( 'NONE',  ( 1.000000000000000000, 0.000000000000000000, 0.000000000000000000 ) ) ;
#2372=CARTESIAN_POINT ( 'NONE',  ( 45.00000000000000000, 515.4878487013597805, -546.7230258972048205 ) ) ;
#2377=CIRCLE ( 'NONE', #1038, 13.69540538389601991 ) ;
#2380=CARTESIAN_POINT ( 'NONE',  ( 45.00000000000000000, 549.5810598491749488, -589.0260321808809749 ) ) ;
#2383=ADVANCED_FACE ( 'NONE', ( #2260 ), #16691, .T. ) ;
#2387=AXIS2_PLACEMENT_3D ( 'NONE', #14335, #7964, #14508 ) ;
#2388=DIRECTION ( 'NONE',  ( 0.000000000000000000, 0.000000000000000000, 1.000000000000000000 ) ) ;
#2392=LINE ( 'NONE', #9186, #6737 ) ;
#2398=EDGE_CURVE ( 'NONE', #4190, #15569, #15055, .T. ) ;
#2406=DIRECTION ( 'NONE',  ( 1.000000000000000000, -0.000000000000000000, 0.000000000000000000 ) ) ;
#2409=AXIS2_PLACEMENT_3D ( 'NONE', #10571, #8076, #6513 ) ;
#2417=ORIENTED_EDGE ( 'NONE', *, *, #4995, .T. ) ;
#2418=VECTOR ( 'NONE', #2970, 1000.000000000000000 ) ;
#2424=PLANE ( 'NONE',  #5028 ) ;
#2425=EDGE_CURVE ( 'NONE', #4130, #7948, #11284, .T. ) ;
#2431=EDGE_LOOP ( 'NONE', ( #6016, #12758 ) ) ;
#2440=FACE_OUTER_BOUND ( 'NONE', #11887, .T. ) ;
#2445=EDGE_CURVE ( 'NONE', #6153, #2950, #1673, .T. ) ;
#2447=ADVANCED_FACE ( 'NONE', ( #4752, #10009, #12659, #984, #2179, #741, #5963, #6203, #13870, #4518, #8800 ), #10091, .T. ) ;
#2450=AXIS2_PLACEMENT_3D ( 'NONE', #15022, #11233, #16643 ) ;
#2451=DIRECTION ( 'NONE',  ( -1.000000000000000000, -0.000000000000000000, -0.000000000000000000 ) ) ;
#2463=ORIENTED_EDGE ( 'NONE', *, *, #8025, .F. ) ;
#2464=CIRCLE ( 'NONE', #6029, 13.69540538389596485 ) ;
#2468=LINE ( 'NONE', #3689, #13835 ) ;
#2471=ORIENTED_EDGE ( 'NONE', *, *, #16722, .F. ) ;
#2480=EDGE_CURVE ( 'NONE', #14915, #3142, #7208, .T. ) ;
#2485=DIRECTION ( 'NONE',  ( 0.000000000000000000, 0.000000000000000000, -1.000000000000000000 ) ) ;
#2489=DIRECTION ( 'NONE',  ( 1.000000000000000000, 0.000000000000000000, 0.000000000000000000 ) ) ;
#2492=DIRECTION ( 'NONE',  ( -1.000000000000000000, 0.000000000000000000, 0.000000000000000000 ) ) ;
#2498=AXIS2_PLACEMENT_3D ( 'NONE', #10868, #1594, #7067 ) ;
#2509=DIRECTION ( 'NONE',  ( 0.000000000000000000, 0.8660254037844432595, -0.4999999999999919509 ) ) ;
#2513=ORIENTED_EDGE ( 'NONE', *, *, #14679, .F. ) ;
#2546=CIRCLE ( 'NONE', #12162, 4.695405383896011919 ) ;
#2547=CARTESIAN_POINT ( 'NONE',  ( 55.99999999999989342, 493.2350855268092573, -585.2659423243250103 ) ) ;
#2552=ORIENTED_EDGE ( 'NONE', *, *, #6044, .T. ) ;
#2554=CIRCLE ( 'NONE', #12174, 13.69540538389601636 ) ;
#2558=ORIENTED_EDGE ( 'NONE', *, *, #2234, .T. ) ;
#2559=DIRECTION ( 'NONE',  ( 0.000000000000000000, 0.000000000000000000, -1.000000000000000000 ) ) ;
#2567=EDGE_LOOP ( 'NONE', ( #12635, #7568, #4570, #4892 ) ) ;
#2569=DIRECTION ( 'NONE',  ( 0.000000000000000000, 0.000000000000000000, 1.000000000000000000 ) ) ;
#2576=ORIENTED_EDGE ( 'NONE', *, *, #9804, .T. ) ;
#2581=ADVANCED_FACE ( 'NONE', ( #15406 ), #5166, .T. ) ;
#2582=ADVANCED_FACE ( 'NONE', ( #6449, #10504 ), #14467, .T. ) ;
#2584=ORIENTED_EDGE ( 'NONE', *, *, #6022, .F. ) ;
#2588=VERTEX_POINT ( 'NONE', #1316 ) ;
#2590=DIRECTION ( 'NONE',  ( 0.000000000000000000, 1.000000000000000000, -1.224646799147353207E-16 ) ) ;
#2604=CIRCLE ( 'NONE', #7252, 13.69540538389601991 ) ;
#2609=CARTESIAN_POINT ( 'NONE',  ( 54.99999999999999289, 515.4878487013597805, -546.7230258972048205 ) ) ;
#2617=AXIS2_PLACEMENT_3D ( 'NONE', #9170, #12175, #12002 ) ;
#2618=ORIENTED_EDGE ( 'NONE', *, *, #9274, .T. ) ;
#2619=ORIENTED_EDGE ( 'NONE', *, *, #14017, .F. ) ;
#2645=AXIS2_PLACEMENT_3D ( 'NONE', #11227, #15181, #15093 ) ;
#2647=AXIS2_PLACEMENT_3D ( 'NONE', #7015, #5812, #13803 ) ;
#2652=CARTESIAN_POINT ( 'NONE',  ( -55.99999999999988631, 515.4878487013597805, -546.7230258972048205 ) ) ;
#2670=ORIENTED_EDGE ( 'NONE', *, *, #8487, .F. ) ;
#2673=ORIENTED_EDGE ( 'NONE', *, *, #2242, .F. ) ;
#2680=ORIENTED_EDGE ( 'NONE', *, *, #12164, .T. ) ;
#2685=CARTESIAN_POINT ( 'NONE',  ( 46.99999999999988631, 473.6663340069158039, -548.2494070140132862 ) ) ;
#2687=CARTESIAN_POINT ( 'NONE',  ( -45.00000000000000000, 523.2161522479888163, -516.5890438806160319 ) ) ;
#2706=DIRECTION ( 'NONE',  ( 0.000000000000000000, 0.000000000000000000, 1.000000000000000000 ) ) ;
#2710=CARTESIAN_POINT ( 'NONE',  ( 55.99999999999989342, 473.6663340069157471, -526.8058340126048051 ) ) ;
#2718=CIRCLE ( 'NONE', #7956, 13.69540538389601991 ) ;
#2720=DIRECTION ( 'NONE',  ( 0.000000000000000000, 0.000000000000000000, 1.000000000000000000 ) ) ;
#2725=CARTESIAN_POINT ( 'NONE',  ( -45.00000000000000000, 549.5810598491746077, -504.4200196135282113 ) ) ;
#2726=EDGE_LOOP ( 'NONE', ( #9475, #6782, #9870, #8577 ) ) ;
#2728=EDGE_CURVE ( 'NONE', #12991, #7948, #2554, .T. ) ;
#2732=CARTESIAN_POINT ( 'NONE',  ( 45.00000000000000000, 549.5810598491746077, -518.1154249974242703 ) ) ;
#2735=FACE_OUTER_BOUND ( 'NONE', #13416, .T. ) ;
#2738=AXIS2_PLACEMENT_3D ( 'NONE', #13478, #4293, #13566 ) ;
#2739=DIRECTION ( 'NONE',  ( 1.000000000000000000, 0.000000000000000000, 0.000000000000000000 ) ) ;
#2751=EDGE_LOOP ( 'NONE', ( #10415, #9482 ) ) ;
#2753=CIRCLE ( 'NONE', #14002, 13.69540538389601991 ) ;
#2761=AXIS2_PLACEMENT_3D ( 'NONE', #1868, #12342, #15010 ) ;
#2772=DIRECTION ( 'NONE',  ( 0.000000000000000000, -0.3420201433256626067, -0.9396926207859105373 ) ) ;
#2773=ORIENTED_EDGE ( 'NONE', *, *, #1817, .T. ) ;
#2775=DIRECTION ( 'NONE',  ( -1.000000000000000000, 0.000000000000000000, -0.000000000000000000 ) ) ;
#2779=DIRECTION ( 'NONE',  ( 0.000000000000000000, 0.000000000000000000, -1.000000000000000000 ) ) ;
#2782=VERTEX_POINT ( 'NONE', #6018 ) ;
#2785=CARTESIAN_POINT ( 'NONE',  ( -55.99999999999989342, 523.2161522479893847, -590.5524132976893270 ) ) ;
#2795=ADVANCED_FACE ( 'NONE', ( #11351 ), #2081, .T. ) ;
#2799=DIRECTION ( 'NONE',  ( 1.000000000000000000, -0.000000000000000000, -0.000000000000000000 ) ) ;
#2804=CARTESIAN_POINT ( 'NONE',  ( 55.99999999999989342, 493.2350855268086320, -494.4847040861889127 ) ) ;
#2813=DIRECTION ( 'NONE',  ( -1.000000000000000000, -0.000000000000000000, -0.000000000000000000 ) ) ;
#2829=CARTESIAN_POINT ( 'NONE',  ( 54.99999999999999289, 645.2345343053611941, -411.3640676610526157 ) ) ;
#2831=ORIENTED_EDGE ( 'NONE', *, *, #7355, .T. ) ;
#2848=TOROIDAL_SURFACE ( 'NONE', #12177, 4.695405383895982609, 9.000000000000000000 ) ;
#2864=DIRECTION ( 'NONE',  ( 0.000000000000000000, 0.8660254037844424824, -0.4999999999999933387 ) ) ;
#2865=DIRECTION ( 'NONE',  ( 0.000000000000000000, 0.000000000000000000, 1.000000000000000000 ) ) ;
#2868=DIRECTION ( 'NONE',  ( 0.000000000000000000, 0.9848077530122061329, 0.1736481776669406840 ) ) ;
#2871=TOROIDAL_SURFACE ( 'NONE', #16851, 4.695405383895982609, 9.000000000000000000 ) ;
#2873=EDGE_CURVE ( 'NONE', #2243, #13962, #11187, .T. ) ;
#2880=ORIENTED_EDGE ( 'NONE', *, *, #13780, .T. ) ;
#2883=CARTESIAN_POINT ( 'NONE',  ( 44.99999999999998579, 515.4878487013597805, -546.7230258972048205 ) ) ;
#2884=LINE ( 'NONE', #1680, #3260 ) ;
#2896=ADVANCED_FACE ( 'NONE', ( #12894 ), #16010, .T. ) ;
#2902=CARTESIAN_POINT ( 'NONE',  ( -45.00000000000000000, 559.9933750504617365, -560.4184312811007658 ) ) ;
#2906=CARTESIAN_POINT ( 'NONE',  ( 46.99999999999988631, 549.5810598491746077, -518.1154249974242703 ) ) ;
#2909=CARTESIAN_POINT ( 'NONE',  ( -55.99999999999988631, 459.5014304922595443, -192.4166442068759579 ) ) ;
#2910=DIRECTION ( 'NONE',  ( 0.000000000000000000, 0.000000000000000000, 1.000000000000000000 ) ) ;
#2921=EDGE_CURVE ( 'NONE', #12389, #6110, #7468, .T. ) ;
#2924=DIRECTION ( 'NONE',  ( -1.000000000000000000, -0.000000000000000000, -0.000000000000000000 ) ) ;
#2936=EDGE_LOOP ( 'NONE', ( #9491, #3975 ) ) ;
#2940=EDGE_LOOP ( 'NONE', ( #9216, #3098, #8494, #12237 ) ) ;
#2942=CIRCLE ( 'NONE', #3457, 9.000000000000007105 ) ;
#2949=DIRECTION ( 'NONE',  ( 0.000000000000000000, 0.000000000000000000, -1.000000000000000000 ) ) ;
#2950=VERTEX_POINT ( 'NONE', #7558 ) ;
#2955=DIRECTION ( 'NONE',  ( -1.000000000000000000, 0.000000000000000000, 0.000000000000000000 ) ) ;
#2957=CARTESIAN_POINT ( 'NONE',  ( -46.99999999999988631, 523.2161522479893847, -590.5524132976893270 ) ) ;
#2965=FACE_OUTER_BOUND ( 'NONE', #3433, .T. ) ;
#2970=DIRECTION ( 'NONE',  ( 1.000000000000000000, -0.000000000000000000, 0.000000000000000000 ) ) ;
#2973=EDGE_CURVE ( 'NONE', #1542, #13093, #5294, .T. ) ;
#2974=DIRECTION ( 'NONE',  ( 1.000000000000000000, 0.000000000000000000, -0.000000000000000000 ) ) ;
#2976=FACE_OUTER_BOUND ( 'NONE', #9851, .T. ) ;
#2978=ORIENTED_EDGE ( 'NONE', *, *, #15739, .T. ) ;
#2988=CARTESIAN_POINT ( 'NONE',  ( -55.99999999999989342, 549.5810598491749488, -570.6352214130889706 ) ) ;
#2989=ORIENTED_EDGE ( 'NONE', *, *, #15059, .T. ) ;
#3004=VERTEX_POINT ( 'NONE', #6263 ) ;
#3005=ADVANCED_FACE ( 'NONE', ( #16752 ), #4982, .T. ) ;
#3019=EDGE_CURVE ( 'NONE', #10713, #6054, #2298, .T. ) ;
#3022=CIRCLE ( 'NONE', #15099, 4.695405383896011919 ) ;
#3023=DIRECTION ( 'NONE',  ( -1.000000000000000000, -0.000000000000000000, 0.000000000000000000 ) ) ;
#3025=PRODUCT_CONTEXT ( 'NONE', #3906, 'mechanical' ) ;
#3028=EDGE_LOOP ( 'NONE', ( #11692, #5339, #443, #16483 ) ) ;
#3031=CARTESIAN_POINT ( 'NONE',  ( -55.99999999999989342, 549.5810598491749488, -575.3306267969850296 ) ) ;
#3042=ORIENTED_EDGE ( 'NONE', *, *, #9516, .F. ) ;
#3049=AXIS2_PLACEMENT_3D ( 'NONE', #4844, #16521, #7242 ) ;
#3055=CIRCLE ( 'NONE', #2498, 9.000000000000007105 ) ;
#3059=CARTESIAN_POINT ( 'NONE',  ( -55.99999999999989342, 523.2161522479888163, -498.1982331128240276 ) ) ;
#3064=VERTEX_POINT ( 'NONE', #14792 ) ;
#3072=EDGE_CURVE ( 'NONE', #3004, #12389, #11908, .T. ) ;
#3076=DIRECTION ( 'NONE',  ( 0.000000000000000000, 0.000000000000000000, 1.000000000000000000 ) ) ;
#3095=DIRECTION ( 'NONE',  ( 1.000000000000000000, 0.000000000000000000, 0.000000000000000000 ) ) ;
#3096=PRODUCT_DEFINITION_CONTEXT ( 'detailed design', #3586, 'design' ) ;
#3098=ORIENTED_EDGE ( 'NONE', *, *, #3197, .T. ) ;
#3110=EDGE_LOOP ( 'NONE', ( #7861, #14209 ) ) ;
#3113=CIRCLE ( 'NONE', #7471, 4.695405383896011919 ) ;
#3129=VECTOR ( 'NONE', #3626, 1000.000000000000000 ) ;
#3130=AXIS2_PLACEMENT_3D ( 'NONE', #10417, #16932, #3891 ) ;
#3133=ORIENTED_EDGE ( 'NONE', *, *, #12664, .T. ) ;
#3142=VERTEX_POINT ( 'NONE', #4713 ) ;
#3150=DIRECTION ( 'NONE',  ( 1.000000000000000000, 0.000000000000000000, 0.000000000000000000 ) ) ;
#3154=DIRECTION ( 'NONE',  ( 1.000000000000000000, 0.000000000000000000, 0.000000000000000000 ) ) ;
#3157=CARTESIAN_POINT ( 'NONE',  ( 46.99999999999988631, 473.6663340069158039, -561.9448123979092315 ) ) ;
#3165=DIRECTION ( 'NONE',  ( 0.000000000000000000, 0.000000000000000000, 1.000000000000000000 ) ) ;
#3169=DIRECTION ( 'NONE',  ( -0.000000000000000000, -1.000000000000000000, 0.000000000000000000 ) ) ;
#3170=CARTESIAN_POINT ( 'NONE',  ( -55.99999999999989342, 493.2350855268092573, -571.5705369404290650 ) ) ;
#3178=ORIENTED_EDGE ( 'NONE', *, *, #4661, .F. ) ;
#3190=DIRECTION ( 'NONE',  ( -1.000000000000000000, -0.000000000000000000, -0.000000000000000000 ) ) ;
#3192=AXIS2_PLACEMENT_3D ( 'NONE', #11494, #1277, #16727 ) ;
#3193=AXIS2_PLACEMENT_3D ( 'NONE', #10914, #14518, #1718 ) ;
#3197=EDGE_CURVE ( 'NONE', #14463, #3860, #14253, .T. ) ;
#3202=VECTOR ( 'NONE', #10879, 1000.000000000000000 ) ;
#3212=CARTESIAN_POINT ( 'NONE',  ( 55.99999999999989342, 473.6663340069158039, -561.9448123979092315 ) ) ;
#3218=CIRCLE ( 'NONE', #6214, 4.695405383896011919 ) ;
#3219=ADVANCED_FACE ( 'NONE', ( #3857 ), #5052, .T. ) ;
#3220=CIRCLE ( 'NONE', #7033, 13.69540538389601991 ) ;
#3223=ORIENTED_EDGE ( 'NONE', *, *, #5649, .F. ) ;
#3230=DIRECTION ( 'NONE',  ( 1.000000000000000000, 0.000000000000000000, 0.000000000000000000 ) ) ;
#3231=DIRECTION ( 'NONE',  ( 0.000000000000000000, 0.000000000000000000, -1.000000000000000000 ) ) ;
#3235=PLANE ( 'NONE',  #5003 ) ;
#3238=DIRECTION ( 'NONE',  ( 1.000000000000000000, 0.000000000000000000, 0.000000000000000000 ) ) ;
#3246=CARTESIAN_POINT ( 'NONE',  ( -55.99999999999989342, 559.9933750504617365, -546.7230258972048205 ) ) ;
#3250=ORIENTED_EDGE ( 'NONE', *, *, #4969, .T. ) ;
#3258=CARTESIAN_POINT ( 'NONE',  ( 54.99999999999999289, 172.2913238082672933, 146.1547335252150788 ) ) ;
#3260=VECTOR ( 'NONE', #5538, 1000.000000000000000 ) ;
#3261=( LENGTH_UNIT ( ) NAMED_UNIT ( * ) SI_UNIT ( .MILLI., .METRE. ) );
#3262=EDGE_LOOP ( 'NONE', ( #907, #5182, #11693, #7882 ) ) ;
#3267=CARTESIAN_POINT ( 'NONE',  ( -55.99999999999989342, 493.2350855268092573, -589.9613477082210693 ) ) ;
#3275=ORIENTED_EDGE ( 'NONE', *, *, #15059, .F. ) ;
#3280=CARTESIAN_POINT ( 'NONE',  ( 0.000000000000000000, 0.000000000000000000, 0.000000000000000000 ) ) ;
#3283=CYLINDRICAL_SURFACE ( 'NONE', #13766, 13.69540538389601991 ) ;
#3286=VERTEX_POINT ( 'NONE', #13134 ) ;
#3296=VERTEX_POINT ( 'NONE', #15700 ) ;
#3306=DIRECTION ( 'NONE',  ( 0.000000000000000000, -0.6930515690182840194, -0.7208880098054721852 ) ) ;
#3308=DIRECTION ( 'NONE',  ( 0.000000000000000000, 0.000000000000000000, -1.000000000000000000 ) ) ;
#3309=EDGE_LOOP ( 'NONE', ( #9892, #7063, #2673, #11481 ) ) ;
#3318=EDGE_CURVE ( 'NONE', #3004, #13474, #16507, .T. ) ;
#3320=CARTESIAN_POINT ( 'NONE',  ( 55.99999999999989342, 523.2161522479893847, -604.2478186815853860 ) ) ;
#3333=DIRECTION ( 'NONE',  ( -1.000000000000000000, 0.000000000000000000, -0.000000000000000000 ) ) ;
#3335=DIRECTION ( 'NONE',  ( 0.000000000000000000, 0.000000000000000000, -1.000000000000000000 ) ) ;
#3338=AXIS2_PLACEMENT_3D ( 'NONE', #4261, #226, #1849 ) ;
#3343=AXIS2_PLACEMENT_3D ( 'NONE', #12340, #7254, #10021 ) ;
#3344=SURFACE_SIDE_STYLE ('',( #15023 ) ) ;
#3351=DIRECTION ( 'NONE',  ( 1.000000000000000000, 0.000000000000000000, 0.000000000000000000 ) ) ;
#3356=AXIS2_PLACEMENT_3D ( 'NONE', #15600, #11816, #7678 ) ;
#3357=DIRECTION ( 'NONE',  ( 1.000000000000000000, -0.000000000000000000, -0.000000000000000000 ) ) ;
#3362=EDGE_CURVE ( 'NONE', #1542, #12590, #5304, .T. ) ;
#3365=CIRCLE ( 'NONE', #5822, 187.4999999999998863 ) ;
#3367=AXIS2_PLACEMENT_3D ( 'NONE', #10725, #437, #8420 ) ;
#3374=AXIS2_PLACEMENT_3D ( 'NONE', #4191, #6575, #9432 ) ;
#3375=DIRECTION ( 'NONE',  ( 0.000000000000000000, 0.3420201433256757073, -0.9396926207859057634 ) ) ;
#3378=AXIS2_PLACEMENT_3D ( 'NONE', #14509, #10467, #10559 ) ;
#3381=( LENGTH_UNIT ( ) NAMED_UNIT ( * ) SI_UNIT ( .MILLI., .METRE. ) );
#3396=ORIENTED_EDGE ( 'NONE', *, *, #280, .T. ) ;
#3403=AXIS2_PLACEMENT_3D ( 'NONE', #10236, #11858, #5677 ) ;
#3404=EDGE_CURVE ( 'NONE', #6185, #1946, #14361, .T. ) ;
#3406=AXIS2_PLACEMENT_3D ( 'NONE', #563, #15145, #11275 ) ;
#3409=CIRCLE ( 'NONE', #12725, 59.99999999999994316 ) ;
#3411=CARTESIAN_POINT ( 'NONE',  ( -45.00000000000000000, 549.5810598491749488, -589.0260321808809749 ) ) ;
#3412=VERTEX_POINT ( 'NONE', #4376 ) ;
#3423=CARTESIAN_POINT ( 'NONE',  ( -46.99999999999988631, 493.2350855268086320, -503.4847040861888559 ) ) ;
#3427=EDGE_CURVE ( 'NONE', #4760, #8117, #3365, .T. ) ;
#3428=CARTESIAN_POINT ( 'NONE',  ( 55.99999999999989342, 549.5810598491746077, -518.1154249974242703 ) ) ;
#3433=EDGE_LOOP ( 'NONE', ( #3223, #13105, #8245, #4845 ) ) ;
#3434=AXIS2_PLACEMENT_3D ( 'NONE', #5823, #11232, #12605 ) ;
#3435=DIRECTION ( 'NONE',  ( 1.000000000000000000, -0.000000000000000000, -0.000000000000000000 ) ) ;
#3438=ORIENTED_EDGE ( 'NONE', *, *, #2480, .F. ) ;
#3445=ORIENTED_EDGE ( 'NONE', *, *, #11586, .T. ) ;
#3455=CARTESIAN_POINT ( 'NONE',  ( 55.99999999999989342, 493.2350855268092573, -571.5705369404290650 ) ) ;
#3457=AXIS2_PLACEMENT_3D ( 'NONE', #546, #5858, #14885 ) ;
#3466=VERTEX_POINT ( 'NONE', #16387 ) ;
#3471=LINE ( 'NONE', #14029, #71 ) ;
#3478=TOROIDAL_SURFACE ( 'NONE', #10330, 4.695405383895982609, 9.000000000000000000 ) ;
#3486=EDGE_LOOP ( 'NONE', ( #16475, #8425 ) ) ;
#3487=CARTESIAN_POINT ( 'NONE',  ( 46.99999999999988631, 493.2350855268086320, -508.1801094700848580 ) ) ;
#3489=CARTESIAN_POINT ( 'NONE',  ( -46.99999999999988631, 549.5810598491749488, -575.3306267969850296 ) ) ;
#3493=LINE ( 'NONE', #12589, #16276 ) ;
#3499=ORIENTED_EDGE ( 'NONE', *, *, #16562, .F. ) ;
#3503=AXIS2_PLACEMENT_3D ( 'NONE', #9970, #3606, #2222 ) ;
#3521=ADVANCED_FACE ( 'NONE', ( #8412 ), #13653, .T. ) ;
#3537=ADVANCED_FACE ( 'NONE', ( #12779 ), #15270, .T. ) ;
#3542=CARTESIAN_POINT ( 'NONE',  ( -45.00000000000000000, 559.9933750504617365, -546.7230258972048205 ) ) ;
#3544=DIRECTION ( 'NONE',  ( -1.000000000000000000, -0.000000000000000000, 0.000000000000000000 ) ) ;
#3545=VERTEX_POINT ( 'NONE', #1088 ) ;
#3551=( NAMED_UNIT ( * ) PLANE_ANGLE_UNIT ( ) SI_UNIT ( $, .RADIAN. ) );
#3552=EDGE_LOOP ( 'NONE', ( #361, #12661, #2131, #12093 ) ) ;
#3563=DIRECTION ( 'NONE',  ( 1.000000000000000000, 0.000000000000000000, -0.000000000000000000 ) ) ;
#3573=EDGE_CURVE ( 'NONE', #16578, #15837, #7685, .T. ) ;
#3583=VERTEX_POINT ( 'NONE', #6062 ) ;
#3586=APPLICATION_CONTEXT ( 'automotive_design' ) ;
#3587=DIRECTION ( 'NONE',  ( 0.000000000000000000, 0.000000000000000000, -1.000000000000000000 ) ) ;
#3589=DIRECTION ( 'NONE',  ( 0.000000000000000000, -0.6930515690182841304, -0.7208880098054721852 ) ) ;
#3595=( NAMED_UNIT ( * ) SI_UNIT ( $, .STERADIAN. ) SOLID_ANGLE_UNIT ( ) );
#3600=DIRECTION ( 'NONE',  ( -1.000000000000000000, -0.000000000000000000, 0.000000000000000000 ) ) ;
#3603=ORIENTED_EDGE ( 'NONE', *, *, #6875, .F. ) ;
#3606=DIRECTION ( 'NONE',  ( -1.000000000000000000, 0.000000000000000000, 0.000000000000000000 ) ) ;
#3609=DIRECTION ( 'NONE',  ( 0.000000000000000000, 0.000000000000000000, -1.000000000000000000 ) ) ;
#3626=DIRECTION ( 'NONE',  ( 1.000000000000000000, -0.000000000000000000, -0.000000000000000000 ) ) ;
#3627=VERTEX_POINT ( 'NONE', #2292 ) ;
#3629=AXIS2_PLACEMENT_3D ( 'NONE', #13827, #4798, #9960 ) ;
#3635=ADVANCED_FACE ( 'NONE', ( #6389 ), #3763, .T. ) ;
#3636=ADVANCED_FACE ( 'NONE', ( #5117 ), #3923, .T. ) ;
#3647=DIRECTION ( 'NONE',  ( -1.000000000000000000, 0.000000000000000000, -0.000000000000000000 ) ) ;
#3650=CARTESIAN_POINT ( 'NONE',  ( 46.99999999999988631, 473.6663340069158039, -561.9448123979092315 ) ) ;
#3663=AXIS2_PLACEMENT_3D ( 'NONE', #254, #14688, #8317 ) ;
#3672=FACE_BOUND ( 'NONE', #15014, .T. ) ;
#3676=DIRECTION ( 'NONE',  ( 0.000000000000000000, 0.000000000000000000, -1.000000000000000000 ) ) ;
#3689=CARTESIAN_POINT ( 'NONE',  ( 55.99999999999989342, 473.6663340069158039, -548.2494070140132862 ) ) ;
#3695=DIRECTION ( 'NONE',  ( 0.000000000000000000, 0.6427876096865299260, 0.7660444431189857850 ) ) ;
#3710=ORIENTED_EDGE ( 'NONE', *, *, #14233, .F. ) ;
#3712=ADVANCED_FACE ( 'NONE', ( #12081 ), #1602, .T. ) ;
#3730=CARTESIAN_POINT ( 'NONE',  ( 55.99999999999989342, 549.5810598491746077, -513.4200196135282113 ) ) ;
#3733=EDGE_CURVE ( 'NONE', #15480, #5615, #3409, .T. ) ;
#3735=LINE ( 'NONE', #6202, #12324 ) ;
#3737=DIRECTION ( 'NONE',  ( 0.000000000000000000, 0.000000000000000000, -1.000000000000000000 ) ) ;
#3747=ORIENTED_EDGE ( 'NONE', *, *, #15007, .F. ) ;
#3748=VERTEX_POINT ( 'NONE', #6649 ) ;
#3752=VECTOR ( 'NONE', #7519, 1000.000000000000000 ) ;
#3753=ORIENTED_EDGE ( 'NONE', *, *, #10058, .T. ) ;
#3760=EDGE_CURVE ( 'NONE', #11607, #3951, #13004, .T. ) ;
#3761=DIRECTION ( 'NONE',  ( 1.000000000000000000, 0.000000000000000000, -0.000000000000000000 ) ) ;
#3763=CYLINDRICAL_SURFACE ( 'NONE', #16568, 13.69540538389601991 ) ;
#3766=AXIS2_PLACEMENT_3D ( 'NONE', #10617, #14569, #13460 ) ;
#3770=ORIENTED_EDGE ( 'NONE', *, *, #2973, .F. ) ;
#3789=ADVANCED_FACE ( 'NONE', ( #12415 ), #12259, .T. ) ;
#3792=DIRECTION ( 'NONE',  ( 0.000000000000000000, 0.000000000000000000, -1.000000000000000000 ) ) ;
#3796=CARTESIAN_POINT ( 'NONE',  ( -46.99999999999988631, 559.9933750504617365, -546.7230258972048205 ) ) ;
#3816=FACE_OUTER_BOUND ( 'NONE', #5430, .T. ) ;
#3821=AXIS2_PLACEMENT_3D ( 'NONE', #16556, #9794, #1959 ) ;
#3827=DIRECTION ( 'NONE',  ( -1.000000000000000000, -0.000000000000000000, -0.000000000000000000 ) ) ;
#3829=CARTESIAN_POINT ( 'NONE',  ( 46.99999999999988631, 523.2161522479888163, -516.5890438806160319 ) ) ;
#3832=FACE_OUTER_BOUND ( 'NONE', #7425, .T. ) ;
#3836=DIRECTION ( 'NONE',  ( 0.000000000000000000, 0.000000000000000000, -1.000000000000000000 ) ) ;
#3841=EDGE_CURVE ( 'NONE', #14813, #9616, #8394, .T. ) ;
#3857=FACE_OUTER_BOUND ( 'NONE', #4618, .T. ) ;
#3860=VERTEX_POINT ( 'NONE', #10880 ) ;
#3864=ADVANCED_FACE ( 'NONE', ( #654 ), #12170, .T. ) ;
#3886=AXIS2_PLACEMENT_3D ( 'NONE', #8478, #13881, #2192 ) ;
#3890=DIRECTION ( 'NONE',  ( 1.000000000000000000, -0.000000000000000000, -0.000000000000000000 ) ) ;
#3891=DIRECTION ( 'NONE',  ( 0.000000000000000000, 0.000000000000000000, -1.000000000000000000 ) ) ;
#3894=DIRECTION ( 'NONE',  ( 1.000000000000000000, 0.000000000000000000, 0.000000000000000000 ) ) ;
#3899=CIRCLE ( 'NONE', #5808, 9.000000000000007105 ) ;
#3906=APPLICATION_CONTEXT ( 'automotive_design' ) ;
#3911=LINE ( 'NONE', #9063, #5850 ) ;
#3922=EDGE_CURVE ( 'NONE', #9423, #5597, #14923, .T. ) ;
#3923=CYLINDRICAL_SURFACE ( 'NONE', #9171, 13.69540538389601991 ) ;
#3927=DIRECTION ( 'NONE',  ( -0.000000000000000000, 1.000000000000000000, -1.224646799147353207E-16 ) ) ;
#3930=DIRECTION ( 'NONE',  ( 0.000000000000000000, 0.000000000000000000, 1.000000000000000000 ) ) ;
#3933=AXIS2_PLACEMENT_3D ( 'NONE', #12306, #8361, #11969 ) ;
#3934=ORIENTED_EDGE ( 'NONE', *, *, #3404, .F. ) ;
#3941=CARTESIAN_POINT ( 'NONE',  ( -45.00000000000000000, 515.4878487013597805, -521.7230258972047068 ) ) ;
#3943=EDGE_CURVE ( 'NONE', #14523, #6600, #11901, .T. ) ;
#3949=CARTESIAN_POINT ( 'NONE',  ( -46.99999999999988631, 473.6663340069158039, -561.9448123979092315 ) ) ;
#3951=VERTEX_POINT ( 'NONE', #11521 ) ;
#3963=TOROIDAL_SURFACE ( 'NONE', #14660, 4.695405383895982609, 9.000000000000000000 ) ;
#3965=EDGE_LOOP ( 'NONE', ( #8553, #2831, #1656, #3970 ) ) ;
#3968=DIRECTION ( 'NONE',  ( 0.000000000000000000, -0.9848077530122090195, 0.1736481776669249744 ) ) ;
#3970=ORIENTED_EDGE ( 'NONE', *, *, #663, .T. ) ;
#3973=ADVANCED_FACE ( 'NONE', ( #7903 ), #108, .T. ) ;
#3975=ORIENTED_EDGE ( 'NONE', *, *, #3404, .T. ) ;
#3976=ORIENTED_EDGE ( 'NONE', *, *, #4061, .T. ) ;
#3977=CARTESIAN_POINT ( 'NONE',  ( 55.99999999999989342, 559.9933750504617365, -560.4184312811007658 ) ) ;
#3980=ORIENTED_EDGE ( 'NONE', *, *, #9582, .F. ) ;
#3985=DIRECTION ( 'NONE',  ( 0.000000000000000000, 0.000000000000000000, -1.000000000000000000 ) ) ;
#3990=DIRECTION ( 'NONE',  ( 0.000000000000000000, 0.000000000000000000, 1.000000000000000000 ) ) ;
#3997=EDGE_LOOP ( 'NONE', ( #12000, #5163 ) ) ;
#3999=CIRCLE ( 'NONE', #7814, 4.695405383896011919 ) ;
#4002=DIRECTION ( 'NONE',  ( -1.000000000000000000, -0.000000000000000000, -0.000000000000000000 ) ) ;
#4007=CYLINDRICAL_SURFACE ( 'NONE', #1151, 187.4999999999998863 ) ;
#4013=DIRECTION ( 'NONE',  ( 0.000000000000000000, 0.000000000000000000, -1.000000000000000000 ) ) ;
#4015=ORIENTED_EDGE ( 'NONE', *, *, #8829, .T. ) ;
#4016=ORIENTED_EDGE ( 'NONE', *, *, #13904, .T. ) ;
#4027=CARTESIAN_POINT ( 'NONE',  ( 46.99999999999988631, 473.6663340069158039, -557.2494070140132862 ) ) ;
#4031=ORIENTED_EDGE ( 'NONE', *, *, #5992, .F. ) ;
#4036=DIRECTION ( 'NONE',  ( 1.000000000000000000, -0.000000000000000000, -0.000000000000000000 ) ) ;
#4043=CARTESIAN_POINT ( 'NONE',  ( 55.99999999999989342, 523.2161522479888163, -502.8936384967199729 ) ) ;
#4045=CARTESIAN_POINT ( 'NONE',  ( 46.99999999999988631, 523.2161522479888163, -498.1982331128240276 ) ) ;
#4061=EDGE_CURVE ( 'NONE', #14215, #3583, #15726, .T. ) ;
#4068=LINE ( 'NONE', #5346, #11599 ) ;
#4074=CARTESIAN_POINT ( 'NONE',  ( 45.00000000000000000, 493.2350855268092573, -585.2659423243250103 ) ) ;
#4081=ORIENTED_EDGE ( 'NONE', *, *, #11376, .T. ) ;
#4085=DIRECTION ( 'NONE',  ( 0.000000000000000000, 0.000000000000000000, 1.000000000000000000 ) ) ;
#4090=DIRECTION ( 'NONE',  ( 0.000000000000000000, 0.000000000000000000, -1.000000000000000000 ) ) ;
#4091=CARTESIAN_POINT ( 'NONE',  ( 45.00000000000000000, 493.2350855268092573, -571.5705369404290650 ) ) ;
#4095=ORIENTED_EDGE ( 'NONE', *, *, #553, .T. ) ;
#4098=AXIS2_PLACEMENT_3D ( 'NONE', #2883, #15930, #4090 ) ;
#4099=CARTESIAN_POINT ( 'NONE',  ( 54.99999999999999289, 515.4878487013597805, -546.7230258972048205 ) ) ;
#4103=DIRECTION ( 'NONE',  ( 0.000000000000000000, 0.000000000000000000, -1.000000000000000000 ) ) ;
#4112=DIRECTION ( 'NONE',  ( 0.000000000000000000, 0.000000000000000000, 1.000000000000000000 ) ) ;
#4117=ORIENTED_EDGE ( 'NONE', *, *, #6866, .F. ) ;
#4128=CIRCLE ( 'NONE', #7674, 9.000000000000007105 ) ;
#4130=VERTEX_POINT ( 'NONE', #14795 ) ;
#4134=EDGE_CURVE ( 'NONE', #3951, #3142, #1565, .T. ) ;
#4135=DIRECTION ( 'NONE',  ( 0.000000000000000000, 0.3420201433256757073, -0.9396926207859057634 ) ) ;
#4139=EDGE_LOOP ( 'NONE', ( #11723, #7955, #8485, #4146 ) ) ;
#4146=ORIENTED_EDGE ( 'NONE', *, *, #13916, .F. ) ;
#4148=ADVANCED_FACE ( 'NONE', ( #8255 ), #15890, .T. ) ;
#4149=EDGE_LOOP ( 'NONE', ( #10693, #16459, #9298, #9445 ) ) ;
#4161=ORIENTED_EDGE ( 'NONE', *, *, #6459, .T. ) ;
#4164=CARTESIAN_POINT ( 'NONE',  ( 55.99999999999989342, 493.2350855268086320, -508.1801094700848580 ) ) ;
#4166=VECTOR ( 'NONE', #6792, 1000.000000000000000 ) ;
#4171=DIRECTION ( 'NONE',  ( 0.000000000000000000, 1.000000000000000000, 1.224646799147353207E-16 ) ) ;
#4179=DIRECTION ( 'NONE',  ( 0.000000000000000000, 0.000000000000000000, 1.000000000000000000 ) ) ;
#4183=CIRCLE ( 'NONE', #6914, 9.000000000000007105 ) ;
#4190=VERTEX_POINT ( 'NONE', #10743 ) ;
#4191=CARTESIAN_POINT ( 'NONE',  ( -55.99999999999989342, 493.2350855268086320, -508.1801094700848580 ) ) ;
#4202=DIRECTION ( 'NONE',  ( 0.000000000000000000, 0.000000000000000000, 1.000000000000000000 ) ) ;
#4203=CARTESIAN_POINT ( 'NONE',  ( -46.99999999999988631, 493.2350855268086320, -508.1801094700848580 ) ) ;
#4205=CARTESIAN_POINT ( 'NONE',  ( -45.00000000000000000, 515.4878487013597805, -571.7230258972048205 ) ) ;
#4216=VERTEX_POINT ( 'NONE', #533 ) ;
#4217=CYLINDRICAL_SURFACE ( 'NONE', #16021, 13.69540538389601991 ) ;
#4228=AXIS2_PLACEMENT_3D ( 'NONE', #14281, #11529, #14203 ) ;
#4231=ADVANCED_FACE ( 'NONE', ( #11173 ), #7374, .T. ) ;
#4233=AXIS2_PLACEMENT_3D ( 'NONE', #12792, #14167, #1358 ) ;
#4238=PRODUCT_DEFINITION_FORMATION_WITH_SPECIFIED_SOURCE ( 'ANY', '', #10283, .NOT_KNOWN. ) ;
#4241=AXIS2_PLACEMENT_3D ( 'NONE', #4489, #9742, #2485 ) ;
#4251=ORIENTED_EDGE ( 'NONE', *, *, #9611, .T. ) ;
#4261=CARTESIAN_POINT ( 'NONE',  ( -55.99999999999989342, 493.2350855268086320, -508.1801094700848580 ) ) ;
#4262=EDGE_CURVE ( 'NONE', #3296, #4760, #7119, .T. ) ;
#4272=DIRECTION ( 'NONE',  ( 0.000000000000000000, 0.000000000000000000, -1.000000000000000000 ) ) ;
#4276=CARTESIAN_POINT ( 'NONE',  ( -46.99999999999988631, 493.2350855268092573, -585.2659423243250103 ) ) ;
#4277=ORIENTED_EDGE ( 'NONE', *, *, #1000, .T. ) ;
#4281=CYLINDRICAL_SURFACE ( 'NONE', #11553, 84.99999999999997158 ) ;
#4284=DIRECTION ( 'NONE',  ( 0.000000000000000000, 0.000000000000000000, 1.000000000000000000 ) ) ;
#4285=ADVANCED_FACE ( 'NONE', ( #8691 ), #6406, .T. ) ;
#4290=DIRECTION ( 'NONE',  ( -1.000000000000000000, -0.000000000000000000, -0.000000000000000000 ) ) ;
#4293=DIRECTION ( 'NONE',  ( -1.000000000000000000, -0.000000000000000000, 0.000000000000000000 ) ) ;
#4297=DIRECTION ( 'NONE',  ( 0.000000000000000000, 0.000000000000000000, -1.000000000000000000 ) ) ;
#4299=VERTEX_POINT ( 'NONE', #5930 ) ;
#4301=FACE_OUTER_BOUND ( 'NONE', #6520, .T. ) ;
#4309=CIRCLE ( 'NONE', #14172, 13.69540538389601991 ) ;
#4310=DIRECTION ( 'NONE',  ( -1.000000000000000000, -0.000000000000000000, -0.000000000000000000 ) ) ;
#4314=DIRECTION ( 'NONE',  ( 1.000000000000000000, 0.000000000000000000, 0.000000000000000000 ) ) ;
#4330=DIRECTION ( 'NONE',  ( 0.000000000000000000, 0.000000000000000000, 1.000000000000000000 ) ) ;
#4335=AXIS2_PLACEMENT_3D ( 'NONE', #3949, #10718, #10905 ) ;
#4337=CARTESIAN_POINT ( 'NONE',  ( 46.99999999999988631, 549.5810598491749488, -561.6352214130889706 ) ) ;
#4350=CARTESIAN_POINT ( 'NONE',  ( 55.99999999999989342, 473.6663340069157471, -531.5012393965008641 ) ) ;
#4362=ADVANCED_FACE ( 'NONE', ( #1037 ), #6975, .T. ) ;
#4373=DIRECTION ( 'NONE',  ( 0.000000000000000000, 0.000000000000000000, 1.000000000000000000 ) ) ;
#4374=DIRECTION ( 'NONE',  ( 1.000000000000000000, -0.000000000000000000, -0.000000000000000000 ) ) ;
#4376=CARTESIAN_POINT ( 'NONE',  ( 49.99999999999999289, 515.4878487013597805, -486.7230258972047636 ) ) ;
#4377=DIRECTION ( 'NONE',  ( 1.000000000000000000, 0.000000000000000000, 0.000000000000000000 ) ) ;
#4381=ADVANCED_FACE ( 'NONE', ( #15460 ), #16903, .T. ) ;
#4382=ADVANCED_FACE ( 'NONE', ( #10469 ), #5878, .T. ) ;
#4390=DIRECTION ( 'NONE',  ( 0.000000000000000000, 0.000000000000000000, 1.000000000000000000 ) ) ;
#4392=CARTESIAN_POINT ( 'NONE',  ( -55.99999999999989342, 559.9933750504617365, -546.7230258972048205 ) ) ;
#4413=DIRECTION ( 'NONE',  ( 0.000000000000000000, 0.000000000000000000, -1.000000000000000000 ) ) ;
#4419=ORIENTED_EDGE ( 'NONE', *, *, #9354, .T. ) ;
#4431=CARTESIAN_POINT ( 'NONE',  ( 46.99999999999988631, 523.2161522479893847, -576.8570079137933817 ) ) ;
#4442=CARTESIAN_POINT ( 'NONE',  ( -55.99999999999988631, 172.2913238082672933, 146.1547335252150788 ) ) ;
#4444=VECTOR ( 'NONE', #15546, 1000.000000000000000 ) ;
#4455=CARTESIAN_POINT ( 'NONE',  ( -54.99999999999999289, 515.4878487013597805, -359.2230258972048773 ) ) ;
#4456=AXIS2_PLACEMENT_3D ( 'NONE', #16179, #16268, #11030 ) ;
#4458=EDGE_CURVE ( 'NONE', #15367, #9686, #11382, .T. ) ;
#4462=EDGE_LOOP ( 'NONE', ( #15817, #9352, #4774, #2195 ) ) ;
#4463=CARTESIAN_POINT ( 'NONE',  ( -46.99999999999988631, 549.5810598491749488, -575.3306267969850296 ) ) ;
#4467=ORIENTED_EDGE ( 'NONE', *, *, #8686, .T. ) ;
#4480=ORIENTED_EDGE ( 'NONE', *, *, #8243, .F. ) ;
#4486=VERTEX_POINT ( 'NONE', #15959 ) ;
#4489=CARTESIAN_POINT ( 'NONE',  ( 46.99999999999988631, 493.2350855268092573, -585.2659423243250103 ) ) ;
#4503=AXIS2_PLACEMENT_3D ( 'NONE', #10406, #1384, #5076 ) ;
#4505=AXIS2_PLACEMENT_3D ( 'NONE', #4707, #7443, #13743 ) ;
#4508=VERTEX_POINT ( 'NONE', #4205 ) ;
#4512=DIRECTION ( 'NONE',  ( 0.000000000000000000, 0.000000000000000000, 1.000000000000000000 ) ) ;
#4518=FACE_BOUND ( 'NONE', #6844, .T. ) ;
#4519=EDGE_LOOP ( 'NONE', ( #11471, #5686, #6192, #8707 ) ) ;
#4522=CARTESIAN_POINT ( 'NONE',  ( 55.99999999999989342, 523.2161522479888163, -502.8936384967199729 ) ) ;
#4530=ADVANCED_FACE ( 'NONE', ( #2735 ), #1366, .T. ) ;
#4535=EDGE_CURVE ( 'NONE', #3545, #4994, #6936, .T. ) ;
#4555=ORIENTED_EDGE ( 'NONE', *, *, #12489, .F. ) ;
#4561=CARTESIAN_POINT ( 'NONE',  ( -55.99999999999989342, 493.2350855268086320, -508.1801094700848580 ) ) ;
#4570=ORIENTED_EDGE ( 'NONE', *, *, #4605, .T. ) ;
#4574=ADVANCED_FACE ( 'NONE', ( #4301 ), #10908, .T. ) ;
#4577=ORIENTED_EDGE ( 'NONE', *, *, #167, .T. ) ;
#4582=EDGE_CURVE ( 'NONE', #7474, #7690, #2050, .T. ) ;
#4602=ORIENTED_EDGE ( 'NONE', *, *, #1199, .T. ) ;
#4605=EDGE_CURVE ( 'NONE', #5350, #13943, #14511, .T. ) ;
#4611=CARTESIAN_POINT ( 'NONE',  ( 54.99999999999999289, 515.4878487013597805, -546.7230258972048205 ) ) ;
#4613=FACE_OUTER_BOUND ( 'NONE', #6757, .T. ) ;
#4617=DIRECTION ( 'NONE',  ( 1.000000000000000000, 0.000000000000000000, 0.000000000000000000 ) ) ;
#4618=EDGE_LOOP ( 'NONE', ( #5595, #2978 ) ) ;
#4619=DIRECTION ( 'NONE',  ( 0.000000000000000000, 0.6468954956981579629, -0.7625786632508376739 ) ) ;
#4629=CARTESIAN_POINT ( 'NONE',  ( 55.99999999999989342, 493.2350855268086320, -521.8755148539809170 ) ) ;
#4630=ORIENTED_EDGE ( 'NONE', *, *, #553, .F. ) ;
#4636=ADVANCED_FACE ( 'NONE', ( #1455 ), #6706, .T. ) ;
#4641=DIRECTION ( 'NONE',  ( 0.000000000000000000, 0.000000000000000000, -1.000000000000000000 ) ) ;
#4644=ADVANCED_FACE ( 'NONE', ( #14942 ), #10039, .F. ) ;
#4654=EDGE_CURVE ( 'NONE', #7744, #12451, #5622, .T. ) ;
#4657=DIRECTION ( 'NONE',  ( 0.000000000000000000, 0.000000000000000000, -1.000000000000000000 ) ) ;
#4661=EDGE_CURVE ( 'NONE', #6401, #14529, #599, .T. ) ;
#4663=EDGE_CURVE ( 'NONE', #13923, #5700, #14962, .T. ) ;
#4666=DIRECTION ( 'NONE',  ( 0.000000000000000000, 0.000000000000000000, -1.000000000000000000 ) ) ;
#4680=CIRCLE ( 'NONE', #2761, 9.000000000000007105 ) ;
#4683=DIRECTION ( 'NONE',  ( 1.000000000000000000, -0.000000000000000000, -0.000000000000000000 ) ) ;
#4684=EDGE_CURVE ( 'NONE', #5265, #1542, #15767, .T. ) ;
#4687=EDGE_LOOP ( 'NONE', ( #9214, #10983, #11510, #6237 ) ) ;
#4691=DIRECTION ( 'NONE',  ( -1.000000000000000000, 0.000000000000000000, 0.000000000000000000 ) ) ;
#4695=AXIS2_PLACEMENT_3D ( 'NONE', #5362, #11725, #4085 ) ;
#4696=FACE_OUTER_BOUND ( 'NONE', #7470, .T. ) ;
#4699=ORIENTED_EDGE ( 'NONE', *, *, #3019, .T. ) ;
#4701=ADVANCED_FACE ( 'NONE', ( #4696 ), #16310, .T. ) ;
#4707=CARTESIAN_POINT ( 'NONE',  ( -46.99999999999988631, 549.5810598491746077, -518.1154249974242703 ) ) ;
#4713=CARTESIAN_POINT ( 'NONE',  ( 45.00000000000000000, 473.6663340069158039, -575.6402177818052905 ) ) ;
#4715=CARTESIAN_POINT ( 'NONE',  ( -55.99999999999989342, 523.2161522479893847, -590.5524132976893270 ) ) ;
#4717=ORIENTED_EDGE ( 'NONE', *, *, #14408, .F. ) ;
#4720=CIRCLE ( 'NONE', #6089, 59.99999999999994316 ) ;
#4723=MECHANICAL_DESIGN_GEOMETRIC_PRESENTATION_REPRESENTATION('',(#14618),#16798);
#4743=CARTESIAN_POINT ( 'NONE',  ( -49.99999999999999289, 515.4878487013597805, -546.7230258972048205 ) ) ;
#4752=FACE_BOUND ( 'NONE', #9265, .T. ) ;
#4758=EDGE_CURVE ( 'NONE', #14998, #11320, #2604, .T. ) ;
#4760=VERTEX_POINT ( 'NONE', #4455 ) ;
#4774=ORIENTED_EDGE ( 'NONE', *, *, #5956, .F. ) ;
#4778=ORIENTED_EDGE ( 'NONE', *, *, #14433, .F. ) ;
#4779=PLANE ( 'NONE',  #10428 ) ;
#4784=EDGE_CURVE ( 'NONE', #10898, #13853, #5034, .T. ) ;
#4792=FACE_OUTER_BOUND ( 'NONE', #10269, .T. ) ;
#4796=ORIENTED_EDGE ( 'NONE', *, *, #2921, .T. ) ;
#4798=DIRECTION ( 'NONE',  ( 1.000000000000000000, 0.000000000000000000, 0.000000000000000000 ) ) ;
#4799=AXIS2_PLACEMENT_3D ( 'NONE', #1878, #8918, #12854 ) ;
#4814=DIRECTION ( 'NONE',  ( 1.000000000000000000, -0.000000000000000000, 0.000000000000000000 ) ) ;
#4816=FACE_OUTER_BOUND ( 'NONE', #13136, .T. ) ;
#4827=ORIENTED_EDGE ( 'NONE', *, *, #7860, .F. ) ;
#4832=ORIENTED_EDGE ( 'NONE', *, *, #4535, .T. ) ;
#4844=CARTESIAN_POINT ( 'NONE',  ( -46.99999999999988631, 493.2350855268092573, -585.2659423243250103 ) ) ;
#4845=ORIENTED_EDGE ( 'NONE', *, *, #4993, .F. ) ;
#4849=DIRECTION ( 'NONE',  ( -1.000000000000000000, -0.000000000000000000, -0.000000000000000000 ) ) ;
#4862=DIRECTION ( 'NONE',  ( 0.000000000000000000, 0.000000000000000000, -1.000000000000000000 ) ) ;
#4868=CARTESIAN_POINT ( 'NONE',  ( -55.99999999999988631, 334.9272574771864015, -321.9943432880672276 ) ) ;
#4874=TOROIDAL_SURFACE ( 'NONE', #7886, 4.695405383895982609, 9.000000000000000000 ) ;
#4881=CYLINDRICAL_SURFACE ( 'NONE', #4233, 13.69540538389601991 ) ;
#4890=CARTESIAN_POINT ( 'NONE',  ( 45.00000000000000000, 523.2161522479888163, -516.5890438806160319 ) ) ;
#4892=ORIENTED_EDGE ( 'NONE', *, *, #9225, .T. ) ;
#4894=AXIS2_PLACEMENT_3D ( 'NONE', #568, #12076, #5714 ) ;
#4918=DIRECTION ( 'NONE',  ( 0.000000000000000000, 0.000000000000000000, -1.000000000000000000 ) ) ;
#4929=TOROIDAL_SURFACE ( 'NONE', #14268, 4.695405383895982609, 9.000000000000000000 ) ;
#4940=CARTESIAN_POINT ( 'NONE',  ( 55.99999999999989342, 549.5810598491746077, -522.8108303813202156 ) ) ;
#4945=DIRECTION ( 'NONE',  ( 0.000000000000000000, 0.000000000000000000, -1.000000000000000000 ) ) ;
#4962=DIRECTION ( 'NONE',  ( 1.000000000000000000, -0.000000000000000000, -0.000000000000000000 ) ) ;
#4967=EDGE_CURVE ( 'NONE', #4486, #13331, #7544, .T. ) ;
#4969=EDGE_CURVE ( 'NONE', #14523, #1188, #14671, .T. ) ;
#4971=ADVANCED_FACE ( 'NONE', ( #6568 ), #13862, .T. ) ;
#4978=DIRECTION ( 'NONE',  ( 0.000000000000000000, -0.8660254037844379305, -0.5000000000000012212 ) ) ;
#4982=CYLINDRICAL_SURFACE ( 'NONE', #3403, 13.69540538389601991 ) ;
#4984=ORIENTED_EDGE ( 'NONE', *, *, #7393, .T. ) ;
#4993=EDGE_CURVE ( 'NONE', #5597, #9423, #3999, .T. ) ;
#4994=VERTEX_POINT ( 'NONE', #15855 ) ;
#4995=EDGE_CURVE ( 'NONE', #7039, #4299, #10031, .T. ) ;
#5003=AXIS2_PLACEMENT_3D ( 'NONE', #7245, #13708, #12499 ) ;
#5009=ORIENTED_EDGE ( 'NONE', *, *, #7725, .T. ) ;
#5013=CIRCLE ( 'NONE', #5275, 13.69540538389601991 ) ;
#5025=FACE_OUTER_BOUND ( 'NONE', #11103, .T. ) ;
#5026=FACE_OUTER_BOUND ( 'NONE', #5882, .T. ) ;
#5028=AXIS2_PLACEMENT_3D ( 'NONE', #6276, #1061, #982 ) ;
#5034=LINE ( 'NONE', #7607, #1234 ) ;
#5050=CARTESIAN_POINT ( 'NONE',  ( -55.99999999999989342, 549.5810598491746077, -513.4200196135282113 ) ) ;
#5052=PLANE ( 'NONE',  #10979 ) ;
#5054=CARTESIAN_POINT ( 'NONE',  ( 55.99999999999989342, 523.2161522479888163, -489.1982331128240276 ) ) ;
#5069=CARTESIAN_POINT ( 'NONE',  ( -46.99999999999988631, 523.2161522479893847, -585.8570079137933817 ) ) ;
#5073=ORIENTED_EDGE ( 'NONE', *, *, #7824, .T. ) ;
#5076=DIRECTION ( 'NONE',  ( 0.000000000000000000, -0.9848077530122086864, 0.1736481776669273613 ) ) ;
#5080=CIRCLE ( 'NONE', #9220, 9.000000000000007105 ) ;
#5089=CARTESIAN_POINT ( 'NONE',  ( 45.00000000000000000, 473.6663340069158039, -561.9448123979092315 ) ) ;
#5097=EDGE_CURVE ( 'NONE', #8336, #1044, #162, .T. ) ;
#5098=CIRCLE ( 'NONE', #11979, 13.69540538389601991 ) ;
#5111=DIRECTION ( 'NONE',  ( -1.000000000000000000, -0.000000000000000000, -0.000000000000000000 ) ) ;
#5117=FACE_OUTER_BOUND ( 'NONE', #9622, .T. ) ;
#5148=ORIENTED_EDGE ( 'NONE', *, *, #16916, .F. ) ;
#5157=ORIENTED_EDGE ( 'NONE', *, *, #6981, .T. ) ;
#5160=DIRECTION ( 'NONE',  ( 0.000000000000000000, 0.000000000000000000, 1.000000000000000000 ) ) ;
#5161=CARTESIAN_POINT ( 'NONE',  ( -55.99999999999989342, 493.2350855268086320, -508.1801094700848580 ) ) ;
#5163=ORIENTED_EDGE ( 'NONE', *, *, #8154, .F. ) ;
#5166=PLANE ( 'NONE',  #15183 ) ;
#5182=ORIENTED_EDGE ( 'NONE', *, *, #12426, .F. ) ;
#5196=CARTESIAN_POINT ( 'NONE',  ( -55.99999999999989342, 549.5810598491746077, -518.1154249974242703 ) ) ;
#5207=ORIENTED_EDGE ( 'NONE', *, *, #8464, .T. ) ;
#5208=DIRECTION ( 'NONE',  ( 1.000000000000000000, 0.000000000000000000, 0.000000000000000000 ) ) ;
#5213=FACE_OUTER_BOUND ( 'NONE', #8952, .T. ) ;
#5222=DIRECTION ( 'NONE',  ( 1.000000000000000000, 0.000000000000000000, -0.000000000000000000 ) ) ;
#5239=ORIENTED_EDGE ( 'NONE', *, *, #2873, .T. ) ;
#5246=AXIS2_PLACEMENT_3D ( 'NONE', #4463, #3435, #12532 ) ;
#5249=ORIENTED_EDGE ( 'NONE', *, *, #663, .F. ) ;
#5251=CARTESIAN_POINT ( 'NONE',  ( 55.99999999999989342, 473.6663340069157471, -545.1966447803968094 ) ) ;
#5265=VERTEX_POINT ( 'NONE', #996 ) ;
#5275=AXIS2_PLACEMENT_3D ( 'NONE', #15826, #1312, #6360 ) ;
#5277=DIRECTION ( 'NONE',  ( 1.000000000000000000, -0.000000000000000000, -0.000000000000000000 ) ) ;
#5294=CIRCLE ( 'NONE', #7222, 9.000000000000007105 ) ;
#5297=EDGE_LOOP ( 'NONE', ( #6039, #9641, #16859, #7301 ) ) ;
#5303=AXIS2_PLACEMENT_3D ( 'NONE', #493, #410, #16114 ) ;
#5304=LINE ( 'NONE', #15787, #15136 ) ;
#5309=AXIS2_PLACEMENT_3D ( 'NONE', #2157, #10150, #4641 ) ;
#5310=ADVANCED_FACE ( 'NONE', ( #8809 ), #9494, .T. ) ;
#5322=FACE_OUTER_BOUND ( 'NONE', #41, .T. ) ;
#5329=AXIS2_PLACEMENT_3D ( 'NONE', #10566, #5222, #10477 ) ;
#5332=ORIENTED_EDGE ( 'NONE', *, *, #8121, .T. ) ;
#5339=ORIENTED_EDGE ( 'NONE', *, *, #2398, .T. ) ;
#5342=DIRECTION ( 'NONE',  ( -1.000000000000000000, 0.000000000000000000, 0.000000000000000000 ) ) ;
#5346=CARTESIAN_POINT ( 'NONE',  ( -55.99999999999989342, 523.2161522479888163, -516.5890438806160319 ) ) ;
#5350=VERTEX_POINT ( 'NONE', #15510 ) ;
#5353=ORIENTED_EDGE ( 'NONE', *, *, #7819, .T. ) ;
#5357=FACE_OUTER_BOUND ( 'NONE', #6218, .T. ) ;
#5362=CARTESIAN_POINT ( 'NONE',  ( -46.99999999999988631, 473.6663340069157471, -531.5012393965008641 ) ) ;
#5363=DIRECTION ( 'NONE',  ( 1.000000000000000000, 0.000000000000000000, 0.000000000000000000 ) ) ;
#5364=EDGE_LOOP ( 'NONE', ( #3438, #7822 ) ) ;
#5377=CIRCLE ( 'NONE', #12796, 13.69540538389601991 ) ;
#5381=DIRECTION ( 'NONE',  ( 0.000000000000000000, 1.000000000000000000, 1.224646799147353207E-16 ) ) ;
#5383=ORIENTED_EDGE ( 'NONE', *, *, #6662, .F. ) ;
#5389=DIRECTION ( 'NONE',  ( -1.000000000000000000, -0.000000000000000000, -0.000000000000000000 ) ) ;
#5391=CIRCLE ( 'NONE', #16647, 4.695405383896011919 ) ;
#5395=ORIENTED_EDGE ( 'NONE', *, *, #12644, .F. ) ;
#5397=FACE_OUTER_BOUND ( 'NONE', #10882, .T. ) ;
#5409=DIRECTION ( 'NONE',  ( 0.000000000000000000, 0.000000000000000000, 1.000000000000000000 ) ) ;
#5413=ORIENTED_EDGE ( 'NONE', *, *, #6337, .F. ) ;
#5424=DIRECTION ( 'NONE',  ( -1.000000000000000000, 0.000000000000000000, 0.000000000000000000 ) ) ;
#5428=AXIS2_PLACEMENT_3D ( 'NONE', #12492, #12827, #1059 ) ;
#5430=EDGE_LOOP ( 'NONE', ( #4117, #16806, #781, #11046 ) ) ;
#5437=ORIENTED_EDGE ( 'NONE', *, *, #10531, .T. ) ;
#5443=ORIENTED_EDGE ( 'NONE', *, *, #8154, .T. ) ;
#5463=CARTESIAN_POINT ( 'NONE',  ( 46.99999999999988631, 523.2161522479893847, -585.8570079137933817 ) ) ;
#5465=DIRECTION ( 'NONE',  ( 0.000000000000000000, 0.000000000000000000, 1.000000000000000000 ) ) ;
#5467=DIRECTION ( 'NONE',  ( 1.000000000000000000, -0.000000000000000000, -0.000000000000000000 ) ) ;
#5476=EDGE_CURVE ( 'NONE', #7039, #16578, #8405, .T. ) ;
#5481=DIRECTION ( 'NONE',  ( 0.000000000000000000, 0.000000000000000000, -1.000000000000000000 ) ) ;
#5484=CARTESIAN_POINT ( 'NONE',  ( 55.99999999999989342, 523.2161522479888163, -498.1982331128240276 ) ) ;
#5493=ADVANCED_FACE ( 'NONE', ( #10603, #5357 ), #6544, .T. ) ;
#5504=AXIS2_PLACEMENT_3D ( 'NONE', #6485, #11744, #13027 ) ;
#5508=ORIENTED_EDGE ( 'NONE', *, *, #4605, .F. ) ;
#5538=DIRECTION ( 'NONE',  ( 0.000000000000000000, -0.6468954956981580739, 0.7625786632508375629 ) ) ;
#5546=CIRCLE ( 'NONE', #8298, 9.000000000000007105 ) ;
#5561=CARTESIAN_POINT ( 'NONE',  ( -55.99999999999989342, 559.9933750504617365, -546.7230258972048205 ) ) ;
#5570=CARTESIAN_POINT ( 'NONE',  ( -55.99999999999989342, 523.2161522479888163, -502.8936384967199729 ) ) ;
#5574=ORIENTED_EDGE ( 'NONE', *, *, #14408, .T. ) ;
#5583=FACE_BOUND ( 'NONE', #14255, .T. ) ;
#5595=ORIENTED_EDGE ( 'NONE', *, *, #5956, .T. ) ;
#5597=VERTEX_POINT ( 'NONE', #5484 ) ;
#5607=EDGE_CURVE ( 'NONE', #2250, #12986, #6947, .T. ) ;
#5612=DIRECTION ( 'NONE',  ( 0.000000000000000000, 0.000000000000000000, 1.000000000000000000 ) ) ;
#5615=VERTEX_POINT ( 'NONE', #7031 ) ;
#5618=ORIENTED_EDGE ( 'NONE', *, *, #957, .F. ) ;
#5621=ADVANCED_FACE ( 'NONE', ( #8244 ), #12032, .T. ) ;
#5622=CIRCLE ( 'NONE', #8648, 13.69540538389601991 ) ;
#5628=ADVANCED_FACE ( 'NONE', ( #12287 ), #13583, .T. ) ;
#5649=EDGE_CURVE ( 'NONE', #13450, #5597, #1819, .T. ) ;
#5657=DIRECTION ( 'NONE',  ( -1.000000000000000000, -0.000000000000000000, 0.000000000000000000 ) ) ;
#5662=AXIS2_PLACEMENT_3D ( 'NONE', #4027, #14844, #3076 ) ;
#5667=DIRECTION ( 'NONE',  ( 0.000000000000000000, 0.000000000000000000, -1.000000000000000000 ) ) ;
#5669=CIRCLE ( 'NONE', #15273, 59.99999999999994316 ) ;
#5670=CARTESIAN_POINT ( 'NONE',  ( 54.99999999999999289, 658.4713480608917280, -425.4301204538002139 ) ) ;
#5677=DIRECTION ( 'NONE',  ( 0.000000000000000000, 0.000000000000000000, -1.000000000000000000 ) ) ;
#5686=ORIENTED_EDGE ( 'NONE', *, *, #9608, .T. ) ;
#5695=EDGE_LOOP ( 'NONE', ( #7456, #662, #4015, #7294 ) ) ;
#5697=DIRECTION ( 'NONE',  ( -1.000000000000000000, -0.000000000000000000, -0.000000000000000000 ) ) ;
#5699=ADVANCED_FACE ( 'NONE', ( #16064 ), #16877, .T. ) ;
#5700=VERTEX_POINT ( 'NONE', #5670 ) ;
#5708=CIRCLE ( 'NONE', #5428, 4.695405383896011919 ) ;
#5714=DIRECTION ( 'NONE',  ( 0.000000000000000000, -0.8660254037844379305, -0.5000000000000012212 ) ) ;
#5715=DIRECTION ( 'NONE',  ( 0.000000000000000000, 0.000000000000000000, 1.000000000000000000 ) ) ;
#5722=VERTEX_POINT ( 'NONE', #8331 ) ;
#5724=EDGE_CURVE ( 'NONE', #3466, #13903, #6693, .T. ) ;
#5733=DIRECTION ( 'NONE',  ( 0.000000000000000000, -0.9848077530122090195, 0.1736481776669249744 ) ) ;
#5751=CARTESIAN_POINT ( 'NONE',  ( -46.99999999999988631, 493.2350855268086320, -508.1801094700848580 ) ) ;
#5754=ORIENTED_EDGE ( 'NONE', *, *, #2398, .F. ) ;
#5757=ORIENTED_EDGE ( 'NONE', *, *, #8624, .F. ) ;
#5766=ORIENTED_EDGE ( 'NONE', *, *, #7002, .T. ) ;
#5771=AXIS2_PLACEMENT_3D ( 'NONE', #2097, #739, #8287 ) ;
#5777=EDGE_CURVE ( 'NONE', #544, #1386, #9961, .T. ) ;
#5781=ORIENTED_EDGE ( 'NONE', *, *, #12665, .T. ) ;
#5791=DIRECTION ( 'NONE',  ( 1.000000000000000000, -0.000000000000000000, 0.000000000000000000 ) ) ;
#5798=EDGE_CURVE ( 'NONE', #3286, #4216, #9793, .T. ) ;
#5804=AXIS2_PLACEMENT_3D ( 'NONE', #1140, #5342, #9127 ) ;
#5808=AXIS2_PLACEMENT_3D ( 'NONE', #174, #3169, #9271 ) ;
#5812=DIRECTION ( 'NONE',  ( -1.000000000000000000, -0.000000000000000000, 0.000000000000000000 ) ) ;
#5817=CIRCLE ( 'NONE', #11570, 4.695405383896011919 ) ;
#5822=AXIS2_PLACEMENT_3D ( 'NONE', #680, #8663, #3335 ) ;
#5823=CARTESIAN_POINT ( 'NONE',  ( 54.99999999999999289, 515.4878487013597805, -546.7230258972048205 ) ) ;
#5836=EDGE_CURVE ( 'NONE', #748, #14972, #5098, .T. ) ;
#5839=VERTEX_POINT ( 'NONE', #12534 ) ;
#5848=CIRCLE ( 'NONE', #1460, 4.695405383895955964 ) ;
#5849=AXIS2_PLACEMENT_3D ( 'NONE', #6979, #5697, #14891 ) ;
#5850=VECTOR ( 'NONE', #14394, 1000.000000000000000 ) ;
#5858=DIRECTION ( 'NONE',  ( 0.000000000000000000, -1.000000000000000000, 0.000000000000000000 ) ) ;
#5877=DIRECTION ( 'NONE',  ( 0.000000000000000000, 0.000000000000000000, 1.000000000000000000 ) ) ;
#5878=TOROIDAL_SURFACE ( 'NONE', #14391, 4.695405383895982609, 9.000000000000000000 ) ;
#5882=EDGE_LOOP ( 'NONE', ( #16218, #10973, #12038, #7279 ) ) ;
#5884=DIRECTION ( 'NONE',  ( 0.000000000000000000, 0.8660254037844424824, -0.4999999999999933387 ) ) ;
#5887=CIRCLE ( 'NONE', #1505, 4.695405383896011919 ) ;
#5889=ORIENTED_EDGE ( 'NONE', *, *, #16493, .T. ) ;
#5892=VECTOR ( 'NONE', #4036, 1000.000000000000000 ) ;
#5910=ORIENTED_EDGE ( 'NONE', *, *, #5607, .F. ) ;
#5912=EDGE_CURVE ( 'NONE', #12736, #9686, #13128, .T. ) ;
#5930=CARTESIAN_POINT ( 'NONE',  ( -55.99999999999989342, 559.9933750504617365, -551.4184312811007658 ) ) ;
#5931=EDGE_CURVE ( 'NONE', #12617, #4130, #6456, .T. ) ;
#5937=ORIENTED_EDGE ( 'NONE', *, *, #11588, .T. ) ;
#5947=ORIENTED_EDGE ( 'NONE', *, *, #6107, .T. ) ;
#5948=ORIENTED_EDGE ( 'NONE', *, *, #7298, .T. ) ;
#5956=EDGE_CURVE ( 'NONE', #6058, #9277, #14996, .T. ) ;
#5963=FACE_BOUND ( 'NONE', #10658, .T. ) ;
#5965=DIRECTION ( 'NONE',  ( 0.000000000000000000, 0.000000000000000000, -1.000000000000000000 ) ) ;
#5967=DIRECTION ( 'NONE',  ( -1.000000000000000000, -0.000000000000000000, 0.000000000000000000 ) ) ;
#5971=ORIENTED_EDGE ( 'NONE', *, *, #6981, .F. ) ;
#5972=CIRCLE ( 'NONE', #10923, 4.695405383896011919 ) ;
#5980=VERTEX_POINT ( 'NONE', #6490 ) ;
#5982=LINE ( 'NONE', #12686, #1961 ) ;
#5984=CARTESIAN_POINT ( 'NONE',  ( 55.99999999999989342, 493.2350855268092573, -598.9613477082210693 ) ) ;
#5989=FILL_AREA_STYLE ('',( #2047 ) ) ;
#5992=EDGE_CURVE ( 'NONE', #1375, #7813, #9235, .T. ) ;
#5995=CARTESIAN_POINT ( 'NONE',  ( -46.99999999999988631, 523.2161522479893847, -590.5524132976893270 ) ) ;
#6002=ORIENTED_EDGE ( 'NONE', *, *, #10058, .F. ) ;
#6009=CARTESIAN_POINT ( 'NONE',  ( 55.99999999999989342, 549.5810598491749488, -580.0260321808809749 ) ) ;
#6016=ORIENTED_EDGE ( 'NONE', *, *, #7829, .T. ) ;
#6018=CARTESIAN_POINT ( 'NONE',  ( -46.99999999999988631, 549.5810598491749488, -561.6352214130889706 ) ) ;
#6020=ORIENTED_EDGE ( 'NONE', *, *, #2425, .F. ) ;
#6022=EDGE_CURVE ( 'NONE', #11607, #6185, #11420, .T. ) ;
#6029=AXIS2_PLACEMENT_3D ( 'NONE', #80, #5467, #4373 ) ;
#6039=ORIENTED_EDGE ( 'NONE', *, *, #3943, .F. ) ;
#6043=CIRCLE ( 'NONE', #16205, 9.000000000000007105 ) ;
#6044=EDGE_CURVE ( 'NONE', #6110, #6925, #8685, .T. ) ;
#6046=CYLINDRICAL_SURFACE ( 'NONE', #15900, 84.99999999999997158 ) ;
#6050=FACE_OUTER_BOUND ( 'NONE', #12305, .T. ) ;
#6054=VERTEX_POINT ( 'NONE', #6924 ) ;
#6058=VERTEX_POINT ( 'NONE', #2988 ) ;
#6059=CARTESIAN_POINT ( 'NONE',  ( -55.99999999999989342, 559.9933750504617365, -546.7230258972048205 ) ) ;
#6062=CARTESIAN_POINT ( 'NONE',  ( 45.00000000000000000, 559.9933750504617365, -560.4184312811007658 ) ) ;
#6065=CIRCLE ( 'NONE', #1955, 9.000000000000007105 ) ;
#6066=DIRECTION ( 'NONE',  ( 0.000000000000000000, 0.000000000000000000, 1.000000000000000000 ) ) ;
#6070=SURFACE_STYLE_USAGE ( .BOTH. , #3344 ) ;
#6072=FACE_OUTER_BOUND ( 'NONE', #12960, .T. ) ;
#6089=AXIS2_PLACEMENT_3D ( 'NONE', #12110, #3095, #5481 ) ;
#6093=DIRECTION ( 'NONE',  ( -1.000000000000000000, -0.000000000000000000, 0.000000000000000000 ) ) ;
#6101=ORIENTED_EDGE ( 'NONE', *, *, #9929, .T. ) ;
#6103=CIRCLE ( 'NONE', #12705, 13.69540538389601991 ) ;
#6105=ORIENTED_EDGE ( 'NONE', *, *, #2234, .F. ) ;
#6106=SHAPE_REPRESENTATION_RELATIONSHIP ( 'NONE' , 'NONE' ,  #1883, #12020 ) ;
#6107=EDGE_CURVE ( 'NONE', #9290, #14252, #11831, .T. ) ;
#6110=VERTEX_POINT ( 'NONE', #2725 ) ;
#6115=ADVANCED_FACE ( 'NONE', ( #6576 ), #10547, .T. ) ;
#6116=AXIS2_PLACEMENT_3D ( 'NONE', #16765, #11621, #4918 ) ;
#6119=AXIS2_PLACEMENT_3D ( 'NONE', #15925, #8200, #2706 ) ;
#6129=ORIENTED_EDGE ( 'NONE', *, *, #16445, .F. ) ;
#6136=ADVANCED_FACE ( 'NONE', ( #1444 ), #6672, .F. ) ;
#6137=DIRECTION ( 'NONE',  ( 0.000000000000000000, 0.000000000000000000, 1.000000000000000000 ) ) ;
#6140=ORIENTED_EDGE ( 'NONE', *, *, #6766, .T. ) ;
#6153=VERTEX_POINT ( 'NONE', #8484 ) ;
#6160=ADVANCED_FACE ( 'NONE', ( #7344 ), #1018, .T. ) ;
#6165=PLANE ( 'NONE',  #247 ) ;
#6176=DIRECTION ( 'NONE',  ( 0.000000000000000000, 0.000000000000000000, -1.000000000000000000 ) ) ;
#6178=DIRECTION ( 'NONE',  ( 0.000000000000000000, 0.000000000000000000, 1.000000000000000000 ) ) ;
#6182=VECTOR ( 'NONE', #6855, 1000.000000000000000 ) ;
#6185=VERTEX_POINT ( 'NONE', #838 ) ;
#6187=ORIENTED_EDGE ( 'NONE', *, *, #7477, .F. ) ;
#6190=VECTOR ( 'NONE', #4374, 1000.000000000000000 ) ;
#6192=ORIENTED_EDGE ( 'NONE', *, *, #5607, .T. ) ;
#6193=EDGE_LOOP ( 'NONE', ( #305, #8984, #5971, #15410 ) ) ;
#6202=CARTESIAN_POINT ( 'NONE',  ( 54.99999999999999289, 515.4878487013597805, -734.2230258972047068 ) ) ;
#6203=FACE_BOUND ( 'NONE', #6874, .T. ) ;
#6214=AXIS2_PLACEMENT_3D ( 'NONE', #14910, #7076, #5715 ) ;
#6218=EDGE_LOOP ( 'NONE', ( #5157, #14670 ) ) ;
#6221=FACE_OUTER_BOUND ( 'NONE', #5695, .T. ) ;
#6231=EDGE_CURVE ( 'NONE', #16287, #3064, #1280, .T. ) ;
#6232=EDGE_CURVE ( 'NONE', #2950, #11164, #14931, .T. ) ;
#6235=DIRECTION ( 'NONE',  ( 1.000000000000000000, 0.000000000000000000, -0.000000000000000000 ) ) ;
#6236=DIRECTION ( 'NONE',  ( 0.000000000000000000, 0.000000000000000000, 1.000000000000000000 ) ) ;
#6237=ORIENTED_EDGE ( 'NONE', *, *, #8673, .F. ) ;
#6241=EDGE_LOOP ( 'NONE', ( #6888, #12741, #5239, #16156 ) ) ;
#6243=CARTESIAN_POINT ( 'NONE',  ( -49.99999999999999289, 515.4878487013597805, -546.7230258972048205 ) ) ;
#6249=EDGE_CURVE ( 'NONE', #15569, #4190, #15275, .T. ) ;
#6262=ORIENTED_EDGE ( 'NONE', *, *, #14550, .F. ) ;
#6263=CARTESIAN_POINT ( 'NONE',  ( -46.99999999999988631, 549.5810598491746077, -531.8108303813202156 ) ) ;
#6264=VERTEX_POINT ( 'NONE', #16300 ) ;
#6266=CIRCLE ( 'NONE', #12056, 9.000000000000007105 ) ;
#6273=AXIS2_PLACEMENT_3D ( 'NONE', #7186, #12443, #15100 ) ;
#6276=CARTESIAN_POINT ( 'NONE',  ( -55.99999999999989342, 523.2161522479888163, -502.8936384967199729 ) ) ;
#6287=ORIENTED_EDGE ( 'NONE', *, *, #3922, .T. ) ;
#6293=VECTOR ( 'NONE', #3563, 1000.000000000000000 ) ;
#6294=DIRECTION ( 'NONE',  ( 0.000000000000000000, 0.000000000000000000, -1.000000000000000000 ) ) ;
#6300=ORIENTED_EDGE ( 'NONE', *, *, #16315, .F. ) ;
#6305=DIRECTION ( 'NONE',  ( 0.000000000000000000, -0.7208880098054721852, 0.6930515690182841304 ) ) ;
#6310=DIRECTION ( 'NONE',  ( 1.000000000000000000, -0.000000000000000000, -0.000000000000000000 ) ) ;
#6317=ADVANCED_FACE ( 'NONE', ( #6221 ), #2198, .F. ) ;
#6325=DIRECTION ( 'NONE',  ( 0.000000000000000000, 0.000000000000000000, 1.000000000000000000 ) ) ;
#6327=ORIENTED_EDGE ( 'NONE', *, *, #2445, .T. ) ;
#6328=DIRECTION ( 'NONE',  ( 0.000000000000000000, 0.000000000000000000, 1.000000000000000000 ) ) ;
#6331=AXIS2_PLACEMENT_3D ( 'NONE', #16491, #713, #9816 ) ;
#6337=EDGE_CURVE ( 'NONE', #544, #14215, #3220, .T. ) ;
#6338=VECTOR ( 'NONE', #5111, 1000.000000000000000 ) ;
#6340=ORIENTED_EDGE ( 'NONE', *, *, #13422, .T. ) ;
#6346=CARTESIAN_POINT ( 'NONE',  ( 46.99999999999988631, 473.6663340069157471, -526.8058340126048051 ) ) ;
#6347=EDGE_LOOP ( 'NONE', ( #3710, #5937, #13572, #2880 ) ) ;
#6348=VERTEX_POINT ( 'NONE', #2687 ) ;
#6349=VECTOR ( 'NONE', #8698, 1000.000000000000000 ) ;
#6350=DIRECTION ( 'NONE',  ( 0.000000000000000000, 0.000000000000000000, -1.000000000000000000 ) ) ;
#6354=AXIS2_PLACEMENT_3D ( 'NONE', #1806, #13658, #16221 ) ;
#6358=FACE_OUTER_BOUND ( 'NONE', #2079, .T. ) ;
#6360=DIRECTION ( 'NONE',  ( 0.000000000000000000, 0.000000000000000000, -1.000000000000000000 ) ) ;
#6364=TOROIDAL_SURFACE ( 'NONE', #9409, 4.695405383895982609, 9.000000000000000000 ) ;
#6369=DIRECTION ( 'NONE',  ( 0.000000000000000000, 0.000000000000000000, -1.000000000000000000 ) ) ;
#6370=EDGE_LOOP ( 'NONE', ( #8342, #307 ) ) ;
#6375=AXIS2_PLACEMENT_3D ( 'NONE', #5089, #13175, #3737 ) ;
#6376=ORIENTED_EDGE ( 'NONE', *, *, #12551, .F. ) ;
#6385=CARTESIAN_POINT ( 'NONE',  ( -54.99999999999999289, 515.4878487013597805, -546.7230258972048205 ) ) ;
#6387=CARTESIAN_POINT ( 'NONE',  ( 55.99999999999989342, 549.5810598491746077, -518.1154249974242703 ) ) ;
#6389=FACE_OUTER_BOUND ( 'NONE', #4519, .T. ) ;
#6398=CARTESIAN_POINT ( 'NONE',  ( 54.99999999999999289, 515.4878487013597805, -734.2230258972047068 ) ) ;
#6399=DIRECTION ( 'NONE',  ( 0.000000000000000000, 0.000000000000000000, 1.000000000000000000 ) ) ;
#6401=VERTEX_POINT ( 'NONE', #921 ) ;
#6406=TOROIDAL_SURFACE ( 'NONE', #12203, 4.695405383895982609, 9.000000000000000000 ) ;
#6410=EDGE_CURVE ( 'NONE', #12590, #14388, #16898, .T. ) ;
#6419=AXIS2_PLACEMENT_3D ( 'NONE', #11068, #7183, #1803 ) ;
#6426=DIRECTION ( 'NONE',  ( 0.000000000000000000, 0.000000000000000000, -1.000000000000000000 ) ) ;
#6432=ORIENTED_EDGE ( 'NONE', *, *, #1710, .F. ) ;
#6440=ORIENTED_EDGE ( 'NONE', *, *, #5836, .F. ) ;
#6449=FACE_OUTER_BOUND ( 'NONE', #9039, .T. ) ;
#6456=CIRCLE ( 'NONE', #10319, 13.69540538389601991 ) ;
#6459=EDGE_CURVE ( 'NONE', #14529, #3296, #15009, .T. ) ;
#6463=EDGE_LOOP ( 'NONE', ( #11160, #576, #12876, #14382 ) ) ;
#6468=CIRCLE ( 'NONE', #10066, 84.99999999999997158 ) ;
#6473=DIRECTION ( 'NONE',  ( 1.000000000000000000, 0.000000000000000000, 0.000000000000000000 ) ) ;
#6475=FACE_BOUND ( 'NONE', #3486, .T. ) ;
#6477=DIRECTION ( 'NONE',  ( -1.000000000000000000, 0.000000000000000000, -0.000000000000000000 ) ) ;
#6479=ORIENTED_EDGE ( 'NONE', *, *, #13215, .F. ) ;
#6484=FACE_OUTER_BOUND ( 'NONE', #988, .T. ) ;
#6485=CARTESIAN_POINT ( 'NONE',  ( 46.99999999999988631, 523.2161522479893847, -590.5524132976893270 ) ) ;
#6489=EDGE_CURVE ( 'NONE', #4994, #9380, #8136, .T. ) ;
#6490=CARTESIAN_POINT ( 'NONE',  ( -55.99999999999989342, 493.2350855268086320, -512.8755148539809170 ) ) ;
#6493=EDGE_CURVE ( 'NONE', #3466, #10713, #2942, .T. ) ;
#6497=FACE_OUTER_BOUND ( 'NONE', #2726, .T. ) ;
#6507=EDGE_CURVE ( 'NONE', #13450, #16590, #8667, .T. ) ;
#6513=DIRECTION ( 'NONE',  ( 0.000000000000000000, 0.000000000000000000, -1.000000000000000000 ) ) ;
#6515=ORIENTED_EDGE ( 'NONE', *, *, #6232, .T. ) ;
#6519=ORIENTED_EDGE ( 'NONE', *, *, #15459, .T. ) ;
#6520=EDGE_LOOP ( 'NONE', ( #16096, #11270, #15534, #2463 ) ) ;
#6527=CIRCLE ( 'NONE', #15331, 13.69540538389601991 ) ;
#6540=CARTESIAN_POINT ( 'NONE',  ( -46.99999999999988631, 523.2161522479893847, -590.5524132976893270 ) ) ;
#6541=VERTEX_POINT ( 'NONE', #6880 ) ;
#6543=ORIENTED_EDGE ( 'NONE', *, *, #4969, .F. ) ;
#6544=PLANE ( 'NONE',  #2352 ) ;
#6546=CIRCLE ( 'NONE', #2450, 13.69540538389601991 ) ;
#6562=AXIS2_PLACEMENT_3D ( 'NONE', #1014, #7771, #4945 ) ;
#6565=CARTESIAN_POINT ( 'NONE',  ( 55.99999999999989342, 473.6663340069157471, -531.5012393965008641 ) ) ;
#6568=FACE_OUTER_BOUND ( 'NONE', #8532, .T. ) ;
#6575=DIRECTION ( 'NONE',  ( -1.000000000000000000, -0.000000000000000000, 0.000000000000000000 ) ) ;
#6576=FACE_OUTER_BOUND ( 'NONE', #8086, .T. ) ;
#6578=DIRECTION ( 'NONE',  ( 0.000000000000000000, -1.000000000000000000, -0.000000000000000000 ) ) ;
#6593=DIRECTION ( 'NONE',  ( 0.000000000000000000, 0.000000000000000000, -1.000000000000000000 ) ) ;
#6600=VERTEX_POINT ( 'NONE', #16498 ) ;
#6607=AXIS2_PLACEMENT_3D ( 'NONE', #7144, #9910, #15321 ) ;
#6611=CIRCLE ( 'NONE', #6891, 59.99999999999994316 ) ;
#6613=FACE_OUTER_BOUND ( 'NONE', #11458, .T. ) ;
#6619=TOROIDAL_SURFACE ( 'NONE', #3629, 4.695405383895982609, 9.000000000000000000 ) ;
#6631=CIRCLE ( 'NONE', #631, 13.69540538389601991 ) ;
#6638=EDGE_LOOP ( 'NONE', ( #4031, #2471 ) ) ;
#6640=AXIS2_PLACEMENT_3D ( 'NONE', #744, #9844, #8470 ) ;
#6649=CARTESIAN_POINT ( 'NONE',  ( -45.00000000000000000, 493.2350855268092573, -598.9613477082210693 ) ) ;
#6662=EDGE_CURVE ( 'NONE', #7948, #12991, #16376, .T. ) ;
#6665=CARTESIAN_POINT ( 'NONE',  ( 45.00000000000000000, 493.2350855268086320, -508.1801094700848580 ) ) ;
#6669=DIRECTION ( 'NONE',  ( 0.000000000000000000, 0.000000000000000000, 1.000000000000000000 ) ) ;
#6672=CYLINDRICAL_SURFACE ( 'NONE', #11154, 25.00000000000002132 ) ;
#6677=DIRECTION ( 'NONE',  ( 0.000000000000000000, 0.000000000000000000, -1.000000000000000000 ) ) ;
#6690=AXIS2_PLACEMENT_3D ( 'NONE', #16659, #10310, #2569 ) ;
#6691=DIRECTION ( 'NONE',  ( 0.000000000000000000, 0.000000000000000000, 1.000000000000000000 ) ) ;
#6693=LINE ( 'NONE', #11948, #6182 ) ;
#6706=TOROIDAL_SURFACE ( 'NONE', #15493, 4.695405383895982609, 9.000000000000000000 ) ;
#6729=ORIENTED_EDGE ( 'NONE', *, *, #7641, .F. ) ;
#6735=DIRECTION ( 'NONE',  ( 1.000000000000000000, -0.000000000000000000, 0.000000000000000000 ) ) ;
#6737=VECTOR ( 'NONE', #2309, 1000.000000000000000 ) ;
#6740=FACE_OUTER_BOUND ( 'NONE', #1987, .T. ) ;
#6757=EDGE_LOOP ( 'NONE', ( #5948, #2280 ) ) ;
#6760=DIRECTION ( 'NONE',  ( -1.000000000000000000, -0.000000000000000000, -0.000000000000000000 ) ) ;
#6763=EDGE_CURVE ( 'NONE', #9290, #6541, #5080, .T. ) ;
#6766=EDGE_CURVE ( 'NONE', #15101, #14286, #16106, .T. ) ;
#6768=DIRECTION ( 'NONE',  ( 1.000000000000000000, 0.000000000000000000, -0.000000000000000000 ) ) ;
#6770=CARTESIAN_POINT ( 'NONE',  ( 55.99999999999989342, 549.5810598491746077, -531.8108303813202156 ) ) ;
#6776=CARTESIAN_POINT ( 'NONE',  ( 55.99999999999989342, 559.9933750504617365, -546.7230258972048205 ) ) ;
#6781=CARTESIAN_POINT ( 'NONE',  ( 49.99999999999999289, 515.4878487013597805, -546.7230258972048205 ) ) ;
#6782=ORIENTED_EDGE ( 'NONE', *, *, #14233, .T. ) ;
#6792=DIRECTION ( 'NONE',  ( 1.000000000000000000, 0.000000000000000000, 0.000000000000000000 ) ) ;
#6804=ORIENTED_EDGE ( 'NONE', *, *, #1228, .T. ) ;
#6812=DIRECTION ( 'NONE',  ( 0.000000000000000000, 1.000000000000000000, -1.224646799147353207E-16 ) ) ;
#6826=AXIS2_PLACEMENT_3D ( 'NONE', #13901, #2126, #7356 ) ;
#6831=ORIENTED_EDGE ( 'NONE', *, *, #12230, .F. ) ;
#6833=AXIS2_PLACEMENT_3D ( 'NONE', #15676, #5277, #1344 ) ;
#6835=ORIENTED_EDGE ( 'NONE', *, *, #1322, .T. ) ;
#6837=DIRECTION ( 'NONE',  ( 0.000000000000000000, 0.000000000000000000, 1.000000000000000000 ) ) ;
#6843=CARTESIAN_POINT ( 'NONE',  ( -45.00000000000000000, 473.6663340069158039, -575.6402177818052905 ) ) ;
#6844=EDGE_LOOP ( 'NONE', ( #6105, #12709 ) ) ;
#6845=DIRECTION ( 'NONE',  ( -1.000000000000000000, -0.000000000000000000, -0.000000000000000000 ) ) ;
#6851=EDGE_CURVE ( 'NONE', #14523, #10388, #12536, .T. ) ;
#6852=ORIENTED_EDGE ( 'NONE', *, *, #13269, .F. ) ;
#6853=FACE_OUTER_BOUND ( 'NONE', #10081, .T. ) ;
#6855=DIRECTION ( 'NONE',  ( -1.000000000000000000, -0.000000000000000000, -0.000000000000000000 ) ) ;
#6857=DIRECTION ( 'NONE',  ( -1.000000000000000000, 0.000000000000000000, 0.000000000000000000 ) ) ;
#6859=DIRECTION ( 'NONE',  ( 0.000000000000000000, 0.000000000000000000, -1.000000000000000000 ) ) ;
#6860=ORIENTED_EDGE ( 'NONE', *, *, #11376, .F. ) ;
#6861=AXIS2_PLACEMENT_3D ( 'NONE', #993, #9053, #14042 ) ;
#6866=EDGE_CURVE ( 'NONE', #10898, #12736, #8429, .T. ) ;
#6872=VECTOR ( 'NONE', #11296, 1000.000000000000000 ) ;
#6874=EDGE_LOOP ( 'NONE', ( #13981, #11018 ) ) ;
#6875=EDGE_CURVE ( 'NONE', #3545, #5839, #2085, .T. ) ;
#6880=CARTESIAN_POINT ( 'NONE',  ( -55.99999999999989342, 523.2161522479893847, -585.8570079137933817 ) ) ;
#6887=CARTESIAN_POINT ( 'NONE',  ( -45.00000000000000000, 523.2161522479893847, -590.5524132976893270 ) ) ;
#6888=ORIENTED_EDGE ( 'NONE', *, *, #3841, .F. ) ;
#6891=AXIS2_PLACEMENT_3D ( 'NONE', #13480, #12015, #253 ) ;
#6892=CIRCLE ( 'NONE', #13225, 13.69540538389601991 ) ;
#6906=DIRECTION ( 'NONE',  ( 1.000000000000000000, 0.000000000000000000, 0.000000000000000000 ) ) ;
#6914=AXIS2_PLACEMENT_3D ( 'NONE', #15466, #11432, #7633 ) ;
#6915=DIRECTION ( 'NONE',  ( -1.000000000000000000, 0.000000000000000000, -0.000000000000000000 ) ) ;
#6918=VECTOR ( 'NONE', #12283, 1000.000000000000000 ) ;
#6924=CARTESIAN_POINT ( 'NONE',  ( 55.99999999999989342, 549.5810598491749488, -570.6352214130889706 ) ) ;
#6925=VERTEX_POINT ( 'NONE', #273 ) ;
#6927=CARTESIAN_POINT ( 'NONE',  ( -46.99999999999988631, 549.5810598491749488, -575.3306267969850296 ) ) ;
#6936=LINE ( 'NONE', #6770, #8382 ) ;
#6943=AXIS2_PLACEMENT_3D ( 'NONE', #16703, #2368, #11645 ) ;
#6947=LINE ( 'NONE', #9457, #8938 ) ;
#6953=CIRCLE ( 'NONE', #392, 13.69540538389601991 ) ;
#6954=CARTESIAN_POINT ( 'NONE',  ( -46.99999999999988631, 549.5810598491746077, -518.1154249974242703 ) ) ;
#6975=TOROIDAL_SURFACE ( 'NONE', #1786, 4.695405383895982609, 9.000000000000000000 ) ;
#6979=CARTESIAN_POINT ( 'NONE',  ( 54.99999999999999289, 515.4878487013597805, -546.7230258972048205 ) ) ;
#6980=ORIENTED_EDGE ( 'NONE', *, *, #1631, .T. ) ;
#6981=EDGE_CURVE ( 'NONE', #4216, #3286, #7550, .T. ) ;
#6992=PLANE ( 'NONE',  #11738 ) ;
#7001=VECTOR ( 'NONE', #6915, 1000.000000000000000 ) ;
#7002=EDGE_CURVE ( 'NONE', #14529, #1196, #2137, .T. ) ;
#7015=CARTESIAN_POINT ( 'NONE',  ( -55.99999999999989342, 473.6663340069157471, -531.5012393965008641 ) ) ;
#7018=CARTESIAN_POINT ( 'NONE',  ( -55.99999999999989342, 559.9933750504617365, -560.4184312811007658 ) ) ;
#7030=AXIS2_PLACEMENT_3D ( 'NONE', #11815, #3761, #3587 ) ;
#7031=CARTESIAN_POINT ( 'NONE',  ( -45.00000000000000000, 515.4878487013597805, -486.7230258972047636 ) ) ;
#7033=AXIS2_PLACEMENT_3D ( 'NONE', #13259, #10674, #4862 ) ;
#7039=VERTEX_POINT ( 'NONE', #9967 ) ;
#7052=CARTESIAN_POINT ( 'NONE',  ( -55.99999999999989342, 523.2161522479893847, -590.5524132976893270 ) ) ;
#7060=ORIENTED_EDGE ( 'NONE', *, *, #8787, .F. ) ;
#7063=ORIENTED_EDGE ( 'NONE', *, *, #14017, .T. ) ;
#7066=AXIS2_PLACEMENT_3D ( 'NONE', #16067, #11769, #3968 ) ;
#7067=DIRECTION ( 'NONE',  ( 0.000000000000000000, 0.000000000000000000, 1.000000000000000000 ) ) ;
#7074=CARTESIAN_POINT ( 'NONE',  ( -46.99999999999988631, 523.2161522479888163, -498.1982331128240276 ) ) ;
#7076=DIRECTION ( 'NONE',  ( -1.000000000000000000, -0.000000000000000000, 0.000000000000000000 ) ) ;
#7078=DIRECTION ( 'NONE',  ( -1.000000000000000000, -0.000000000000000000, -0.000000000000000000 ) ) ;
#7086=CYLINDRICAL_SURFACE ( 'NONE', #15929, 13.69540538389601991 ) ;
#7090=EDGE_CURVE ( 'NONE', #6600, #5722, #12372, .T. ) ;
#7104=CYLINDRICAL_SURFACE ( 'NONE', #11504, 13.69540538389601991 ) ;
#7112=FACE_OUTER_BOUND ( 'NONE', #14395, .T. ) ;
#7115=ORIENTED_EDGE ( 'NONE', *, *, #2028, .F. ) ;
#7117=EDGE_LOOP ( 'NONE', ( #6287, #288 ) ) ;
#7119=LINE ( 'NONE', #11091, #10279 ) ;
#7125=ORIENTED_EDGE ( 'NONE', *, *, #8132, .F. ) ;
#7144=CARTESIAN_POINT ( 'NONE',  ( -46.99999999999988631, 549.5810598491749488, -580.0260321808809749 ) ) ;
#7151=ORIENTED_EDGE ( 'NONE', *, *, #12980, .T. ) ;
#7157=DIRECTION ( 'NONE',  ( 0.000000000000000000, 0.000000000000000000, 1.000000000000000000 ) ) ;
#7159=ORIENTED_EDGE ( 'NONE', *, *, #12644, .T. ) ;
#7164=CARTESIAN_POINT ( 'NONE',  ( -55.99999999999989342, 523.2161522479893847, -590.5524132976893270 ) ) ;
#7181=EDGE_CURVE ( 'NONE', #9156, #614, #2392, .T. ) ;
#7183=DIRECTION ( 'NONE',  ( -1.000000000000000000, 0.000000000000000000, -0.000000000000000000 ) ) ;
#7185=CIRCLE ( 'NONE', #4456, 13.69540538389601991 ) ;
#7186=CARTESIAN_POINT ( 'NONE',  ( 46.99999999999988631, 559.9933750504617365, -546.7230258972048205 ) ) ;
#7195=COLOUR_RGB ( '', 0.08235294, 0.09019608, 0.10196078) ;
#7206=EDGE_CURVE ( 'NONE', #15036, #3627, #10585, .T. ) ;
#7208=CIRCLE ( 'NONE', #6375, 13.69540538389601991 ) ;
#7220=DIRECTION ( 'NONE',  ( 0.000000000000000000, -0.3420201433256626067, -0.9396926207859105373 ) ) ;
#7222=AXIS2_PLACEMENT_3D ( 'NONE', #6346, #2590, #11772 ) ;
#7242=DIRECTION ( 'NONE',  ( 0.000000000000000000, 0.000000000000000000, 1.000000000000000000 ) ) ;
#7245=CARTESIAN_POINT ( 'NONE',  ( -55.99999999999988631, 173.0499717945046996, 146.7982946275220968 ) ) ;
#7247=VECTOR ( 'NONE', #4683, 1000.000000000000000 ) ;
#7249=EDGE_LOOP ( 'NONE', ( #4095, #4577 ) ) ;
#7252=AXIS2_PLACEMENT_3D ( 'NONE', #8322, #13656, #6066 ) ;
#7254=DIRECTION ( 'NONE',  ( 1.000000000000000000, 0.000000000000000000, 0.000000000000000000 ) ) ;
#7266=CARTESIAN_POINT ( 'NONE',  ( -55.99999999999989342, 523.2161522479888163, -507.5890438806159750 ) ) ;
#7270=EDGE_LOOP ( 'NONE', ( #14389, #7319, #8894, #14473 ) ) ;
#7275=AXIS2_PLACEMENT_3D ( 'NONE', #4045, #442, #1555 ) ;
#7279=ORIENTED_EDGE ( 'NONE', *, *, #12252, .T. ) ;
#7281=ADVANCED_FACE ( 'NONE', ( #7698 ), #15618, .T. ) ;
#7283=DIRECTION ( 'NONE',  ( 0.000000000000000000, 0.000000000000000000, 1.000000000000000000 ) ) ;
#7293=PLANE ( 'NONE',  #8447 ) ;
#7294=ORIENTED_EDGE ( 'NONE', *, *, #167, .F. ) ;
#7298=EDGE_CURVE ( 'NONE', #15837, #4299, #472, .T. ) ;
#7301=ORIENTED_EDGE ( 'NONE', *, *, #193, .F. ) ;
#7302=AXIS2_PLACEMENT_3D ( 'NONE', #4611, #1871, #11058 ) ;
#7311=ORIENTED_EDGE ( 'NONE', *, *, #5931, .T. ) ;
#7315=TOROIDAL_SURFACE ( 'NONE', #1016, 4.695405383895982609, 9.000000000000000000 ) ;
#7319=ORIENTED_EDGE ( 'NONE', *, *, #13904, .F. ) ;
#7326=DIRECTION ( 'NONE',  ( 1.000000000000000000, 0.000000000000000000, -0.000000000000000000 ) ) ;
#7338=EDGE_CURVE ( 'NONE', #13962, #9616, #6468, .T. ) ;
#7339=CARTESIAN_POINT ( 'NONE',  ( -46.99999999999988631, 493.2350855268092573, -589.9613477082210693 ) ) ;
#7344=FACE_OUTER_BOUND ( 'NONE', #4462, .T. ) ;
#7346=DIRECTION ( 'NONE',  ( -1.000000000000000000, 0.000000000000000000, 0.000000000000000000 ) ) ;
#7353=ORIENTED_EDGE ( 'NONE', *, *, #7338, .F. ) ;
#7355=EDGE_CURVE ( 'NONE', #2950, #6153, #4309, .T. ) ;
#7356=DIRECTION ( 'NONE',  ( 0.000000000000000000, -0.6427876096865372535, 0.7660444431189797898 ) ) ;
#7357=ORIENTED_EDGE ( 'NONE', *, *, #16414, .T. ) ;
#7358=VECTOR ( 'NONE', #3154, 1000.000000000000000 ) ;
#7363=FACE_OUTER_BOUND ( 'NONE', #9368, .T. ) ;
#7364=DIRECTION ( 'NONE',  ( 1.000000000000000000, -0.000000000000000000, 0.000000000000000000 ) ) ;
#7366=ORIENTED_EDGE ( 'NONE', *, *, #12331, .T. ) ;
#7374=CYLINDRICAL_SURFACE ( 'NONE', #10004, 13.69540538389601991 ) ;
#7380=DIRECTION ( 'NONE',  ( 1.000000000000000000, -0.000000000000000000, 0.000000000000000000 ) ) ;
#7387=ADVANCED_FACE ( 'NONE', ( #8056 ), #3478, .T. ) ;
#7392=EDGE_CURVE ( 'NONE', #4190, #3286, #8312, .T. ) ;
#7393=EDGE_CURVE ( 'NONE', #7039, #14972, #1447, .T. ) ;
#7395=ADVANCED_FACE ( 'NONE', ( #12014 ), #9348, .F. ) ;
#7397=AXIS2_PLACEMENT_3D ( 'NONE', #6887, #14638, #2868 ) ;
#7423=DIRECTION ( 'NONE',  ( 0.000000000000000000, 0.000000000000000000, -1.000000000000000000 ) ) ;
#7425=EDGE_LOOP ( 'NONE', ( #5757, #16403, #10944, #1008 ) ) ;
#7430=LINE ( 'NONE', #5984, #2129 ) ;
#7435=CLOSED_SHELL ( 'NONE', ( #13816, #4382, #8463, #2383, #16257, #12121, #5310, #11057, #16192, #4574, #8533, #8373, #4381, #10119, #10147, #8376, #4701, #7696, #2896, #6160, #14492, #8866, #14652, #4362, #8497, #14714, #10364, #8767, #11808, #14046, #2168, #3636, #3789, #10423, #12553, #12319, #4644, #13692, #7395, #1125, #8990, #1409, #7281, #1609, #13937, #2582, #1874, #15060, #5493, #2171, #15683, #7551, #6317, #2447, #6136, #9637, #12788, #13933, #6115, #12454, #16954, #4231, #10145, #11468, #13934, #10645, #4148, #3005, #2581, #9895, #8349, #13815, #3219, #5699, #990, #8466, #10029, #4636, #4971, #12359, #7387, #15395, #407, #5621, #3864, #441, #10945, #3973, #3712, #3521, #10345, #1577, #13767, #2795, #456, #4530, #3635, #10873, #5628, #13322, #9589, #15381, #1638, #12857, #7923, #7602, #4285, #14429, #618, #12973, #3537, #720, #14860, #9174 ) ) ;
#7436=AXIS2_PLACEMENT_3D ( 'NONE', #2547, #6235, #12941 ) ;
#7440=CIRCLE ( 'NONE', #5246, 13.69540538389601991 ) ;
#7441=DIRECTION ( 'NONE',  ( -1.000000000000000000, -0.000000000000000000, -0.000000000000000000 ) ) ;
#7443=DIRECTION ( 'NONE',  ( 1.000000000000000000, -0.000000000000000000, -0.000000000000000000 ) ) ;
#7447=AXIS2_PLACEMENT_3D ( 'NONE', #13402, #1621, #14769 ) ;
#7450=VECTOR ( 'NONE', #9909, 1000.000000000000000 ) ;
#7456=ORIENTED_EDGE ( 'NONE', *, *, #1483, .F. ) ;
#7458=AXIS2_PLACEMENT_3D ( 'NONE', #12413, #14911, #5884 ) ;
#7466=AXIS2_PLACEMENT_3D ( 'NONE', #12576, #7326, #14842 ) ;
#7468=LINE ( 'NONE', #12734, #3129 ) ;
#7470=EDGE_LOOP ( 'NONE', ( #11714, #4832, #14191, #9292 ) ) ;
#7471=AXIS2_PLACEMENT_3D ( 'NONE', #8189, #13443, #5612 ) ;
#7472=AXIS2_PLACEMENT_3D ( 'NONE', #502, #1869, #13884 ) ;
#7474=VERTEX_POINT ( 'NONE', #7266 ) ;
#7477=EDGE_CURVE ( 'NONE', #6600, #14523, #5377, .T. ) ;
#7478=DIRECTION ( 'NONE',  ( 1.000000000000000000, 0.000000000000000000, 0.000000000000000000 ) ) ;
#7496=TOROIDAL_SURFACE ( 'NONE', #16817, 4.695405383895982609, 9.000000000000000000 ) ;
#7518=CIRCLE ( 'NONE', #134, 13.69540538389601991 ) ;
#7519=DIRECTION ( 'NONE',  ( 0.000000000000000000, -0.6468954956981580739, 0.7625786632508375629 ) ) ;
#7521=AXIS2_PLACEMENT_3D ( 'NONE', #3428, #848, #8666 ) ;
#7523=DIRECTION ( 'NONE',  ( -1.000000000000000000, -0.000000000000000000, 0.000000000000000000 ) ) ;
#7530=ORIENTED_EDGE ( 'NONE', *, *, #4758, .T. ) ;
#7544=CIRCLE ( 'NONE', #151, 9.000000000000007105 ) ;
#7550=CIRCLE ( 'NONE', #1545, 84.99999999999997158 ) ;
#7551=ADVANCED_FACE ( 'NONE', ( #9071, #6475, #11475, #14307, #3672, #7856, #16708, #8820, #13113, #1340, #5025 ), #15429, .T. ) ;
#7558=CARTESIAN_POINT ( 'NONE',  ( -46.99999999999988631, 493.2350855268092573, -571.5705369404290650 ) ) ;
#7562=EDGE_LOOP ( 'NONE', ( #15140, #12848, #7353, #11001 ) ) ;
#7564=AXIS2_PLACEMENT_3D ( 'NONE', #5561, #427, #2910 ) ;
#7565=AXIS2_PLACEMENT_3D ( 'NONE', #12790, #2304, #11749 ) ;
#7568=ORIENTED_EDGE ( 'NONE', *, *, #786, .T. ) ;
#7574=CIRCLE ( 'NONE', #13368, 9.000000000000007105 ) ;
#7576=AXIS2_PLACEMENT_3D ( 'NONE', #9481, #294, #2949 ) ;
#7589=AXIS2_PLACEMENT_3D ( 'NONE', #9189, #4377, #9533 ) ;
#7596=DIRECTION ( 'NONE',  ( -1.000000000000000000, 0.000000000000000000, 0.000000000000000000 ) ) ;
#7598=DIRECTION ( 'NONE',  ( 1.000000000000000000, 0.000000000000000000, 0.000000000000000000 ) ) ;
#7602=ADVANCED_FACE ( 'NONE', ( #10440 ), #738, .T. ) ;
#7607=CARTESIAN_POINT ( 'NONE',  ( -55.99999999999988631, 460.1944820612779381, -191.6957561970704660 ) ) ;
#7608=EDGE_CURVE ( 'NONE', #15367, #10898, #12932, .T. ) ;
#7626=VERTEX_POINT ( 'NONE', #9587 ) ;
#7633=DIRECTION ( 'NONE',  ( 0.000000000000000000, 0.000000000000000000, -1.000000000000000000 ) ) ;
#7636=EDGE_LOOP ( 'NONE', ( #15196, #9084 ) ) ;
#7641=EDGE_CURVE ( 'NONE', #5615, #15480, #5669, .T. ) ;
#7645=CARTESIAN_POINT ( 'NONE',  ( 46.99999999999988631, 493.2350855268086320, -508.1801094700848580 ) ) ;
#7646=ORIENTED_EDGE ( 'NONE', *, *, #13780, .F. ) ;
#7654=DIRECTION ( 'NONE',  ( 0.000000000000000000, 0.000000000000000000, -1.000000000000000000 ) ) ;
#7658=LINE ( 'NONE', #9141, #8709 ) ;
#7662=ORIENTED_EDGE ( 'NONE', *, *, #2311, .F. ) ;
#7667=ORIENTED_EDGE ( 'NONE', *, *, #4661, .T. ) ;
#7671=ORIENTED_EDGE ( 'NONE', *, *, #6231, .F. ) ;
#7674=AXIS2_PLACEMENT_3D ( 'NONE', #14098, #14263, #13145 ) ;
#7678=DIRECTION ( 'NONE',  ( 0.000000000000000000, 0.000000000000000000, 1.000000000000000000 ) ) ;
#7685=CIRCLE ( 'NONE', #12138, 9.000000000000007105 ) ;
#7686=DIRECTION ( 'NONE',  ( 1.000000000000000000, 0.000000000000000000, 0.000000000000000000 ) ) ;
#7688=CARTESIAN_POINT ( 'NONE',  ( -46.99999999999988631, 559.9933750504617365, -546.7230258972048205 ) ) ;
#7690=VERTEX_POINT ( 'NONE', #3059 ) ;
#7694=EDGE_LOOP ( 'NONE', ( #16145, #4602, #12925, #79 ) ) ;
#7696=ADVANCED_FACE ( 'NONE', ( #6740 ), #8126, .T. ) ;
#7698=FACE_OUTER_BOUND ( 'NONE', #4149, .T. ) ;
#7701=AXIS2_PLACEMENT_3D ( 'NONE', #4164, #9403, #14651 ) ;
#7715=AXIS2_PLACEMENT_3D ( 'NONE', #2732, #11934, #15789 ) ;
#7721=EDGE_CURVE ( 'NONE', #12617, #12991, #15849, .T. ) ;
#7722=DIRECTION ( 'NONE',  ( 0.000000000000000000, 0.000000000000000000, -1.000000000000000000 ) ) ;
#7725=EDGE_CURVE ( 'NONE', #3951, #11607, #15551, .T. ) ;
#7728=ORIENTED_EDGE ( 'NONE', *, *, #6763, .F. ) ;
#7734=EDGE_LOOP ( 'NONE', ( #2619, #9810, #13672, #3499 ) ) ;
#7735=FACE_OUTER_BOUND ( 'NONE', #8862, .T. ) ;
#7737=AXIS2_PLACEMENT_3D ( 'NONE', #13309, #14582, #8049 ) ;
#7744=VERTEX_POINT ( 'NONE', #4091 ) ;
#7753=AXIS2_PLACEMENT_3D ( 'NONE', #2609, #3894, #11789 ) ;
#7757=AXIS2_PLACEMENT_3D ( 'NONE', #13698, #3150, #4657 ) ;
#7763=CARTESIAN_POINT ( 'NONE',  ( -46.99999999999988631, 559.9933750504617365, -533.0276205133087615 ) ) ;
#7765=CARTESIAN_POINT ( 'NONE',  ( -46.99999999999988631, 549.5810598491749488, -589.0260321808809749 ) ) ;
#7769=CARTESIAN_POINT ( 'NONE',  ( -45.00000000000000000, 515.4878487013597805, -546.7230258972048205 ) ) ;
#7771=DIRECTION ( 'NONE',  ( -1.000000000000000000, -0.000000000000000000, -0.000000000000000000 ) ) ;
#7772=ORIENTED_EDGE ( 'NONE', *, *, #12489, .T. ) ;
#7777=AXIS2_PLACEMENT_3D ( 'NONE', #14952, #608, #16400 ) ;
#7785=DIRECTION ( 'NONE',  ( 1.000000000000000000, 0.000000000000000000, -0.000000000000000000 ) ) ;
#7786=ORIENTED_EDGE ( 'NONE', *, *, #7721, .F. ) ;
#7795=CARTESIAN_POINT ( 'NONE',  ( 46.99999999999988631, 549.5810598491749488, -575.3306267969850296 ) ) ;
#7813=VERTEX_POINT ( 'NONE', #15073 ) ;
#7814=AXIS2_PLACEMENT_3D ( 'NONE', #1432, #13205, #14495 ) ;
#7819=EDGE_CURVE ( 'NONE', #2588, #16404, #12276, .T. ) ;
#7822=ORIENTED_EDGE ( 'NONE', *, *, #16414, .F. ) ;
#7824=EDGE_CURVE ( 'NONE', #2782, #6058, #7574, .T. ) ;
#7829=EDGE_CURVE ( 'NONE', #3064, #16287, #3218, .T. ) ;
#7831=DIRECTION ( 'NONE',  ( 0.000000000000000000, 0.000000000000000000, -1.000000000000000000 ) ) ;
#7836=ORIENTED_EDGE ( 'NONE', *, *, #2335, .T. ) ;
#7847=CARTESIAN_POINT ( 'NONE',  ( 46.99999999999988631, 559.9933750504617365, -551.4184312811007658 ) ) ;
#7856=FACE_BOUND ( 'NONE', #10940, .T. ) ;
#7860=EDGE_CURVE ( 'NONE', #7626, #13903, #10902, .T. ) ;
#7861=ORIENTED_EDGE ( 'NONE', *, *, #12053, .F. ) ;
#7871=DIRECTION ( 'NONE',  ( -1.000000000000000000, 0.000000000000000000, 0.000000000000000000 ) ) ;
#7880=FACE_OUTER_BOUND ( 'NONE', #8187, .T. ) ;
#7882=ORIENTED_EDGE ( 'NONE', *, *, #1000, .F. ) ;
#7884=DIRECTION ( 'NONE',  ( -1.000000000000000000, 0.000000000000000000, 0.000000000000000000 ) ) ;
#7886=AXIS2_PLACEMENT_3D ( 'NONE', #1540, #1800, #12278 ) ;
#7903=FACE_OUTER_BOUND ( 'NONE', #7117, .T. ) ;
#7908=EDGE_LOOP ( 'NONE', ( #2584, #15579, #3396, #3934 ) ) ;
#7916=CIRCLE ( 'NONE', #4098, 25.00000000000002132 ) ;
#7920=CARTESIAN_POINT ( 'NONE',  ( -54.99999999999999289, 515.4878487013597805, -734.2230258972047068 ) ) ;
#7923=ADVANCED_FACE ( 'NONE', ( #2348 ), #7315, .T. ) ;
#7926=CARTESIAN_POINT ( 'NONE',  ( -46.99999999999988631, 523.2161522479893847, -595.2478186815853860 ) ) ;
#7942=CIRCLE ( 'NONE', #16718, 4.695405383896011919 ) ;
#7948=VERTEX_POINT ( 'NONE', #13007 ) ;
#7952=DIRECTION ( 'NONE',  ( 0.000000000000000000, 0.000000000000000000, -1.000000000000000000 ) ) ;
#7955=ORIENTED_EDGE ( 'NONE', *, *, #15990, .F. ) ;
#7956=AXIS2_PLACEMENT_3D ( 'NONE', #10527, #10616, #54 ) ;
#7962=CARTESIAN_POINT ( 'NONE',  ( -54.99999999999999289, 515.4878487013597805, -546.7230258972048205 ) ) ;
#7964=DIRECTION ( 'NONE',  ( -1.000000000000000000, -0.000000000000000000, -0.000000000000000000 ) ) ;
#7975=TOROIDAL_SURFACE ( 'NONE', #4695, 4.695405383895982609, 9.000000000000000000 ) ;
#7993=AXIS2_PLACEMENT_3D ( 'NONE', #11931, #12096, #6677 ) ;
#7994=AXIS2_PLACEMENT_3D ( 'NONE', #7688, #12861, #3930 ) ;
#8006=CARTESIAN_POINT ( 'NONE',  ( -55.99999999999989342, 473.6663340069158039, -566.6402177818052905 ) ) ;
#8009=AXIS2_PLACEMENT_3D ( 'NONE', #10033, #4691, #13977 ) ;
#8025=EDGE_CURVE ( 'NONE', #8101, #7626, #7658, .T. ) ;
#8045=AXIS2_PLACEMENT_3D ( 'NONE', #10831, #6857, #12115 ) ;
#8049=DIRECTION ( 'NONE',  ( 0.000000000000000000, 0.000000000000000000, -1.000000000000000000 ) ) ;
#8050=AXIS2_PLACEMENT_3D ( 'NONE', #3212, #632, #3375 ) ;
#8052=DIRECTION ( 'NONE',  ( 0.000000000000000000, -0.6427876096865372535, 0.7660444431189797898 ) ) ;
#8056=FACE_OUTER_BOUND ( 'NONE', #8911, .T. ) ;
#8070=PLANE ( 'NONE',  #11033 ) ;
#8073=DIRECTION ( 'NONE',  ( 1.000000000000000000, 0.000000000000000000, -0.000000000000000000 ) ) ;
#8076=DIRECTION ( 'NONE',  ( -1.000000000000000000, -0.000000000000000000, -0.000000000000000000 ) ) ;
#8078=ORIENTED_EDGE ( 'NONE', *, *, #7355, .F. ) ;
#8081=ORIENTED_EDGE ( 'NONE', *, *, #4134, .T. ) ;
#8086=EDGE_LOOP ( 'NONE', ( #9796, #4277 ) ) ;
#8094=CARTESIAN_POINT ( 'NONE',  ( -55.99999999999988631, 459.5014304922595443, -192.4166442068759579 ) ) ;
#8101=VERTEX_POINT ( 'NONE', #4337 ) ;
#8104=DIRECTION ( 'NONE',  ( -1.000000000000000000, 0.000000000000000000, -0.000000000000000000 ) ) ;
#8116=CARTESIAN_POINT ( 'NONE',  ( 46.99999999999988631, 523.2161522479888163, -502.8936384967199729 ) ) ;
#8117=VERTEX_POINT ( 'NONE', #7920 ) ;
#8118=DIRECTION ( 'NONE',  ( -1.000000000000000000, -0.000000000000000000, -0.000000000000000000 ) ) ;
#8121=EDGE_CURVE ( 'NONE', #11164, #3748, #11162, .T. ) ;
#8126=CYLINDRICAL_SURFACE ( 'NONE', #8415, 13.69540538389601991 ) ;
#8132=EDGE_CURVE ( 'NONE', #1946, #6185, #5391, .T. ) ;
#8136=CIRCLE ( 'NONE', #13900, 13.69540538389601991 ) ;
#8147=AXIS2_PLACEMENT_3D ( 'NONE', #8725, #1860, #9843 ) ;
#8151=CARTESIAN_POINT ( 'NONE',  ( -46.99999999999988631, 493.2350855268086320, -508.1801094700848580 ) ) ;
#8154=EDGE_CURVE ( 'NONE', #12451, #7744, #2377, .T. ) ;
#8160=TOROIDAL_SURFACE ( 'NONE', #15564, 4.695405383895982609, 9.000000000000000000 ) ;
#8167=CARTESIAN_POINT ( 'NONE',  ( -54.99999999999999289, 515.4878487013597805, -546.7230258972048205 ) ) ;
#8187=EDGE_LOOP ( 'NONE', ( #5781, #13897, #5443, #130 ) ) ;
#8189=CARTESIAN_POINT ( 'NONE',  ( -55.99999999999989342, 549.5810598491746077, -518.1154249974242703 ) ) ;
#8190=ORIENTED_EDGE ( 'NONE', *, *, #2480, .T. ) ;
#8195=CIRCLE ( 'NONE', #12851, 4.695405383896011919 ) ;
#8200=DIRECTION ( 'NONE',  ( -1.000000000000000000, 0.000000000000000000, 0.000000000000000000 ) ) ;
#8212=DIRECTION ( 'NONE',  ( 0.000000000000000000, 0.000000000000000000, 1.000000000000000000 ) ) ;
#8216=CARTESIAN_POINT ( 'NONE',  ( 46.99999999999988631, 549.5810598491746077, -513.4200196135282113 ) ) ;
#8228=DIRECTION ( 'NONE',  ( 0.000000000000000000, 0.000000000000000000, 1.000000000000000000 ) ) ;
#8230=CARTESIAN_POINT ( 'NONE',  ( 55.99999999999989342, 549.5810598491749488, -575.3306267969850296 ) ) ;
#8243=EDGE_CURVE ( 'NONE', #12863, #15101, #16654, .T. ) ;
#8244=FACE_OUTER_BOUND ( 'NONE', #7636, .T. ) ;
#8245=ORIENTED_EDGE ( 'NONE', *, *, #10938, .T. ) ;
#8246=DIRECTION ( 'NONE',  ( 0.000000000000000000, 0.000000000000000000, -1.000000000000000000 ) ) ;
#8254=ORIENTED_EDGE ( 'NONE', *, *, #1199, .F. ) ;
#8255=FACE_OUTER_BOUND ( 'NONE', #12839, .T. ) ;
#8264=EDGE_LOOP ( 'NONE', ( #10326, #1793, #3747, #7728 ) ) ;
#8270=ORIENTED_EDGE ( 'NONE', *, *, #5777, .F. ) ;
#8275=EDGE_LOOP ( 'NONE', ( #3770, #11151, #13822, #12836 ) ) ;
#8287=DIRECTION ( 'NONE',  ( 0.000000000000000000, 0.000000000000000000, -1.000000000000000000 ) ) ;
#8291=DIRECTION ( 'NONE',  ( 0.000000000000000000, 0.000000000000000000, 1.000000000000000000 ) ) ;
#8293=CARTESIAN_POINT ( 'NONE',  ( -55.99999999999989342, 493.2350855268086320, -508.1801094700848580 ) ) ;
#8295=ORIENTED_EDGE ( 'NONE', *, *, #2445, .F. ) ;
#8298=AXIS2_PLACEMENT_3D ( 'NONE', #10565, #1552, #5667 ) ;
#8301=CARTESIAN_POINT ( 'NONE',  ( -54.99999999999999289, 515.4878487013597805, -461.7230258972048205 ) ) ;
#8302=CIRCLE ( 'NONE', #7458, 13.69540538389598083 ) ;
#8312=LINE ( 'NONE', #13315, #13898 ) ;
#8317=DIRECTION ( 'NONE',  ( 0.000000000000000000, 0.000000000000000000, -1.000000000000000000 ) ) ;
#8322=CARTESIAN_POINT ( 'NONE',  ( -46.99999999999988631, 473.6663340069158039, -561.9448123979092315 ) ) ;
#8323=CIRCLE ( 'NONE', #3933, 9.000000000000007105 ) ;
#8324=EDGE_CURVE ( 'NONE', #4508, #12483, #765, .T. ) ;
#8330=DIRECTION ( 'NONE',  ( 1.000000000000000000, 0.000000000000000000, -0.000000000000000000 ) ) ;
#8331=CARTESIAN_POINT ( 'NONE',  ( 45.00000000000000000, 493.2350855268086320, -521.8755148539809170 ) ) ;
#8336=VERTEX_POINT ( 'NONE', #4890 ) ;
#8342=ORIENTED_EDGE ( 'NONE', *, *, #9225, .F. ) ;
#8349=ADVANCED_FACE ( 'NONE', ( #12799 ), #7293, .T. ) ;
#8356=CARTESIAN_POINT ( 'NONE',  ( 55.99999999999989342, 473.6663340069157471, -531.5012393965008641 ) ) ;
#8357=ORIENTED_EDGE ( 'NONE', *, *, #9390, .T. ) ;
#8361=DIRECTION ( 'NONE',  ( 0.000000000000000000, -1.000000000000000000, 0.000000000000000000 ) ) ;
#8373=ADVANCED_FACE ( 'NONE', ( #7880 ), #85, .T. ) ;
#8376=ADVANCED_FACE ( 'NONE', ( #6497 ), #11933, .T. ) ;
#8379=ORIENTED_EDGE ( 'NONE', *, *, #1228, .F. ) ;
#8382=VECTOR ( 'NONE', #10721, 1000.000000000000000 ) ;
#8386=CARTESIAN_POINT ( 'NONE',  ( 46.99999999999988631, 473.6663340069157471, -517.8058340126048051 ) ) ;
#8388=CARTESIAN_POINT ( 'NONE',  ( -45.00000000000000000, 473.6663340069158039, -561.9448123979092315 ) ) ;
#8389=FACE_OUTER_BOUND ( 'NONE', #12356, .T. ) ;
#8394=LINE ( 'NONE', #12502, #9995 ) ;
#8405=CIRCLE ( 'NONE', #10587, 13.69540538389601991 ) ;
#8408=FACE_OUTER_BOUND ( 'NONE', #8275, .T. ) ;
#8412=FACE_OUTER_BOUND ( 'NONE', #8596, .T. ) ;
#8415=AXIS2_PLACEMENT_3D ( 'NONE', #11906, #1517, #8291 ) ;
#8420=DIRECTION ( 'NONE',  ( 0.000000000000000000, 0.000000000000000000, 1.000000000000000000 ) ) ;
#8425=ORIENTED_EDGE ( 'NONE', *, *, #12331, .F. ) ;
#8429=LINE ( 'NONE', #16231, #9503 ) ;
#8433=ORIENTED_EDGE ( 'NONE', *, *, #14884, .T. ) ;
#8447=AXIS2_PLACEMENT_3D ( 'NONE', #4715, #8763, #16482 ) ;
#8460=DIRECTION ( 'NONE',  ( -1.000000000000000000, -0.000000000000000000, -0.000000000000000000 ) ) ;
#8463=ADVANCED_FACE ( 'NONE', ( #5213 ), #13382, .T. ) ;
#8464=EDGE_CURVE ( 'NONE', #11320, #14998, #15840, .T. ) ;
#8466=ADVANCED_FACE ( 'NONE', ( #14770 ), #8160, .T. ) ;
#8470=DIRECTION ( 'NONE',  ( 0.000000000000000000, 0.000000000000000000, -1.000000000000000000 ) ) ;
#8478=CARTESIAN_POINT ( 'NONE',  ( -55.99999999999989342, 493.2350855268092573, -585.2659423243250103 ) ) ;
#8482=AXIS2_PLACEMENT_3D ( 'NONE', #15071, #15151, #3308 ) ;
#8484=CARTESIAN_POINT ( 'NONE',  ( -46.99999999999988631, 493.2350855268092573, -598.9613477082210693 ) ) ;
#8485=ORIENTED_EDGE ( 'NONE', *, *, #14517, .T. ) ;
#8487=EDGE_CURVE ( 'NONE', #1995, #13331, #12296, .T. ) ;
#8492=DIRECTION ( 'NONE',  ( 0.000000000000000000, 0.000000000000000000, 1.000000000000000000 ) ) ;
#8494=ORIENTED_EDGE ( 'NONE', *, *, #12830, .T. ) ;
#8497=ADVANCED_FACE ( 'NONE', ( #9704 ), #4874, .T. ) ;
#8504=CARTESIAN_POINT ( 'NONE',  ( 55.99999999999989342, 493.2350855268086320, -508.1801094700848580 ) ) ;
#8511=CIRCLE ( 'NONE', #9306, 84.99999999999997158 ) ;
#8532=EDGE_LOOP ( 'NONE', ( #14264, #8078, #1650, #2513 ) ) ;
#8533=ADVANCED_FACE ( 'NONE', ( #13733 ), #2293, .T. ) ;
#8543=ORIENTED_EDGE ( 'NONE', *, *, #1322, .F. ) ;
#8549=DIRECTION ( 'NONE',  ( 0.000000000000000000, 0.000000000000000000, -1.000000000000000000 ) ) ;
#8550=CIRCLE ( 'NONE', #7994, 13.69540538389601991 ) ;
#8552=CARTESIAN_POINT ( 'NONE',  ( 54.99999999999999289, 515.4878487013597805, -546.7230258972048205 ) ) ;
#8553=ORIENTED_EDGE ( 'NONE', *, *, #6232, .F. ) ;
#8563=FACE_OUTER_BOUND ( 'NONE', #2567, .T. ) ;
#8571=ORIENTED_EDGE ( 'NONE', *, *, #193, .T. ) ;
#8576=CARTESIAN_POINT ( 'NONE',  ( 55.99999999999989342, 549.5810598491749488, -575.3306267969850296 ) ) ;
#8577=ORIENTED_EDGE ( 'NONE', *, *, #1292, .F. ) ;
#8580=AXIS2_PLACEMENT_3D ( 'NONE', #11411, #16644, #6236 ) ;
#8581=EDGE_CURVE ( 'NONE', #15297, #15749, #507, .T. ) ;
#8583=CYLINDRICAL_SURFACE ( 'NONE', #3821, 13.69540538389601991 ) ;
#8591=DIRECTION ( 'NONE',  ( 0.000000000000000000, 0.000000000000000000, 1.000000000000000000 ) ) ;
#8596=EDGE_LOOP ( 'NONE', ( #12497, #11445 ) ) ;
#8611=ORIENTED_EDGE ( 'NONE', *, *, #8882, .F. ) ;
#8617=CIRCLE ( 'NONE', #7757, 59.99999999999994316 ) ;
#8624=EDGE_CURVE ( 'NONE', #11329, #12451, #7430, .T. ) ;
#8639=DIRECTION ( 'NONE',  ( 1.000000000000000000, 0.000000000000000000, 0.000000000000000000 ) ) ;
#8648=AXIS2_PLACEMENT_3D ( 'NONE', #16555, #15021, #15190 ) ;
#8663=DIRECTION ( 'NONE',  ( 1.000000000000000000, 0.000000000000000000, 0.000000000000000000 ) ) ;
#8666=DIRECTION ( 'NONE',  ( 0.000000000000000000, 0.000000000000000000, 1.000000000000000000 ) ) ;
#8667=CIRCLE ( 'NONE', #15249, 13.69540538389601991 ) ;
#8670=EDGE_LOOP ( 'NONE', ( #6002, #12978, #6101, #10657 ) ) ;
#8673=EDGE_CURVE ( 'NONE', #6054, #10713, #5972, .T. ) ;
#8679=CARTESIAN_POINT ( 'NONE',  ( 55.99999999999989342, 493.2350855268092573, -589.9613477082210693 ) ) ;
#8683=AXIS2_PLACEMENT_3D ( 'NONE', #10735, #3190, #16068 ) ;
#8685=CIRCLE ( 'NONE', #10877, 13.69540538389598439 ) ;
#8686=EDGE_CURVE ( 'NONE', #2250, #11869, #13115, .T. ) ;
#8691=FACE_OUTER_BOUND ( 'NONE', #1241, .T. ) ;
#8693=DIRECTION ( 'NONE',  ( 0.000000000000000000, 0.000000000000000000, 1.000000000000000000 ) ) ;
#8698=DIRECTION ( 'NONE',  ( -1.000000000000000000, -0.000000000000000000, -0.000000000000000000 ) ) ;
#8700=ORIENTED_EDGE ( 'NONE', *, *, #7477, .T. ) ;
#8707=ORIENTED_EDGE ( 'NONE', *, *, #14259, .T. ) ;
#8709=VECTOR ( 'NONE', #14379, 1000.000000000000000 ) ;
#8725=CARTESIAN_POINT ( 'NONE',  ( 44.99999999999998579, 515.4878487013597805, -546.7230258972048205 ) ) ;
#8736=LINE ( 'NONE', #9935, #11883 ) ;
#8739=CARTESIAN_POINT ( 'NONE',  ( -46.99999999999988631, 549.5810598491749488, -575.3306267969850296 ) ) ;
#8741=DIRECTION ( 'NONE',  ( 0.000000000000000000, 0.000000000000000000, 1.000000000000000000 ) ) ;
#8754=ORIENTED_EDGE ( 'NONE', *, *, #6493, .F. ) ;
#8756=DIRECTION ( 'NONE',  ( 0.000000000000000000, 0.000000000000000000, -1.000000000000000000 ) ) ;
#8758=DIRECTION ( 'NONE',  ( 0.000000000000000000, 0.000000000000000000, -1.000000000000000000 ) ) ;
#8763=DIRECTION ( 'NONE',  ( -1.000000000000000000, 0.000000000000000000, 0.000000000000000000 ) ) ;
#8766=DIRECTION ( 'NONE',  ( 1.000000000000000000, 0.000000000000000000, -0.000000000000000000 ) ) ;
#8767=ADVANCED_FACE ( 'NONE', ( #14404 ), #15526, .T. ) ;
#8777=ORIENTED_EDGE ( 'NONE', *, *, #5931, .F. ) ;
#8781=CIRCLE ( 'NONE', #2738, 13.69540538389601991 ) ;
#8787=EDGE_CURVE ( 'NONE', #12214, #13093, #7942, .T. ) ;
#8792=AXIS2_PLACEMENT_3D ( 'NONE', #7074, #12578, #1926 ) ;
#8800=FACE_OUTER_BOUND ( 'NONE', #10322, .T. ) ;
#8809=FACE_OUTER_BOUND ( 'NONE', #5297, .T. ) ;
#8820=FACE_BOUND ( 'NONE', #2751, .T. ) ;
#8829=EDGE_CURVE ( 'NONE', #5615, #8853, #16196, .T. ) ;
#8842=ORIENTED_EDGE ( 'NONE', *, *, #5836, .T. ) ;
#8847=EDGE_LOOP ( 'NONE', ( #2618, #5947, #1243, #5508 ) ) ;
#8851=CIRCLE ( 'NONE', #15981, 9.000000000000007105 ) ;
#8853=VERTEX_POINT ( 'NONE', #16115 ) ;
#8861=CARTESIAN_POINT ( 'NONE',  ( -45.00000000000000000, 473.6663340069157471, -531.5012393965008641 ) ) ;
#8862=EDGE_LOOP ( 'NONE', ( #12815, #9734, #6129, #12586 ) ) ;
#8866=ADVANCED_FACE ( 'NONE', ( #2976 ), #4929, .T. ) ;
#8875=ORIENTED_EDGE ( 'NONE', *, *, #9929, .F. ) ;
#8882=EDGE_CURVE ( 'NONE', #13599, #12411, #13449, .T. ) ;
#8893=CIRCLE ( 'NONE', #401, 4.695405383896011919 ) ;
#8894=ORIENTED_EDGE ( 'NONE', *, *, #3573, .T. ) ;
#8901=AXIS2_PLACEMENT_3D ( 'NONE', #6954, #3357, #11330 ) ;
#8905=VECTOR ( 'NONE', #9215, 1000.000000000000000 ) ;
#8911=EDGE_LOOP ( 'NONE', ( #2066, #16832, #5073, #1399 ) ) ;
#8915=CARTESIAN_POINT ( 'NONE',  ( 55.99999999999989342, 493.2350855268092573, -585.2659423243250103 ) ) ;
#8918=DIRECTION ( 'NONE',  ( 1.000000000000000000, 0.000000000000000000, 0.000000000000000000 ) ) ;
#8925=AXIS2_PLACEMENT_3D ( 'NONE', #415, #10448, #15772 ) ;
#8930=FACE_OUTER_BOUND ( 'NONE', #10485, .T. ) ;
#8938=VECTOR ( 'NONE', #4310, 1000.000000000000000 ) ;
#8946=AXIS2_PLACEMENT_3D ( 'NONE', #15782, #13392, #14503 ) ;
#8952=EDGE_LOOP ( 'NONE', ( #2166, #302, #16484, #2115 ) ) ;
#8971=AXIS2_PLACEMENT_3D ( 'NONE', #14188, #14352, #10321 ) ;
#8972=CARTESIAN_POINT ( 'NONE',  ( -55.99999999999989342, 493.2350855268092573, -585.2659423243250103 ) ) ;
#8976=ORIENTED_EDGE ( 'NONE', *, *, #15481, .T. ) ;
#8984=ORIENTED_EDGE ( 'NONE', *, *, #7392, .T. ) ;
#8990=ADVANCED_FACE ( 'NONE', ( #15003 ), #6046, .F. ) ;
#8993=DIRECTION ( 'NONE',  ( 0.000000000000000000, 0.000000000000000000, 1.000000000000000000 ) ) ;
#8999=CARTESIAN_POINT ( 'NONE',  ( 55.99999999999989342, 523.2161522479893847, -590.5524132976893270 ) ) ;
#9013=CARTESIAN_POINT ( 'NONE',  ( 46.99999999999988631, 473.6663340069157471, -536.1966447803968094 ) ) ;
#9014=FACE_OUTER_BOUND ( 'NONE', #14619, .T. ) ;
#9020=ORIENTED_EDGE ( 'NONE', *, *, #12053, .T. ) ;
#9022=CIRCLE ( 'NONE', #4894, 13.69540538389598794 ) ;
#9025=ORIENTED_EDGE ( 'NONE', *, *, #12830, .F. ) ;
#9029=ORIENTED_EDGE ( 'NONE', *, *, #12568, .F. ) ;
#9031=AXIS2_PLACEMENT_3D ( 'NONE', #12751, #8639, #649 ) ;
#9039=EDGE_LOOP ( 'NONE', ( #4161, #13096, #13012, #14272, #881, #7667 ) ) ;
#9053=DIRECTION ( 'NONE',  ( 1.000000000000000000, -0.000000000000000000, 0.000000000000000000 ) ) ;
#9063=CARTESIAN_POINT ( 'NONE',  ( 55.99999999999989342, 549.5810598491746077, -504.4200196135282113 ) ) ;
#9071=FACE_BOUND ( 'NONE', #15949, .T. ) ;
#9072=DIRECTION ( 'NONE',  ( -1.000000000000000000, -0.000000000000000000, 0.000000000000000000 ) ) ;
#9077=EDGE_CURVE ( 'NONE', #3627, #15036, #3022, .T. ) ;
#9084=ORIENTED_EDGE ( 'NONE', *, *, #7206, .T. ) ;
#9111=CARTESIAN_POINT ( 'NONE',  ( 45.00000000000000000, 549.5810598491746077, -504.4200196135282113 ) ) ;
#9121=DIRECTION ( 'NONE',  ( -1.000000000000000000, 0.000000000000000000, -0.000000000000000000 ) ) ;
#9122=VERTEX_POINT ( 'NONE', #11795 ) ;
#9127=DIRECTION ( 'NONE',  ( 0.000000000000000000, 0.000000000000000000, 1.000000000000000000 ) ) ;
#9140=ORIENTED_EDGE ( 'NONE', *, *, #1631, .F. ) ;
#9141=CARTESIAN_POINT ( 'NONE',  ( 55.99999999999989342, 549.5810598491749488, -561.6352214130889706 ) ) ;
#9146=ORIENTED_EDGE ( 'NONE', *, *, #786, .F. ) ;
#9156=VERTEX_POINT ( 'NONE', #15580 ) ;
#9157=CARTESIAN_POINT ( 'NONE',  ( 54.99999999999999289, 658.4713480608917280, -425.4301204538002139 ) ) ;
#9161=DIRECTION ( 'NONE',  ( 0.000000000000000000, 0.000000000000000000, -1.000000000000000000 ) ) ;
#9163=DIRECTION ( 'NONE',  ( 1.000000000000000000, 0.000000000000000000, 0.000000000000000000 ) ) ;
#9164=AXIS2_PLACEMENT_3D ( 'NONE', #14374, #16682, #7654 ) ;
#9170=CARTESIAN_POINT ( 'NONE',  ( -46.99999999999988631, 493.2350855268092573, -585.2659423243250103 ) ) ;
#9171=AXIS2_PLACEMENT_3D ( 'NONE', #10443, #15851, #1520 ) ;
#9173=DIRECTION ( 'NONE',  ( 0.000000000000000000, 0.000000000000000000, -1.000000000000000000 ) ) ;
#9174=ADVANCED_FACE ( 'NONE', ( #3816 ), #12837, .F. ) ;
#9175=CARTESIAN_POINT ( 'NONE',  ( -46.99999999999988631, 473.6663340069157471, -536.1966447803968094 ) ) ;
#9186=CARTESIAN_POINT ( 'NONE',  ( 45.00000000000000000, 515.4878487013597805, -606.7230258972047068 ) ) ;
#9189=CARTESIAN_POINT ( 'NONE',  ( 46.99999999999988631, 523.2161522479893847, -590.5524132976893270 ) ) ;
#9214=ORIENTED_EDGE ( 'NONE', *, *, #9354, .F. ) ;
#9215=DIRECTION ( 'NONE',  ( -1.000000000000000000, -0.000000000000000000, -0.000000000000000000 ) ) ;
#9216=ORIENTED_EDGE ( 'NONE', *, *, #13909, .T. ) ;
#9220=AXIS2_PLACEMENT_3D ( 'NONE', #5069, #14522, #7722 ) ;
#9222=AXIS2_PLACEMENT_3D ( 'NONE', #524, #14862, #4390 ) ;
#9225=EDGE_CURVE ( 'NONE', #13943, #14252, #1931, .T. ) ;
#9235=CIRCLE ( 'NONE', #7565, 13.69540538389597017 ) ;
#9239=EDGE_LOOP ( 'NONE', ( #5353, #6980, #15359, #3275 ) ) ;
#9250=DIRECTION ( 'NONE',  ( 1.000000000000000000, -0.000000000000000000, -0.000000000000000000 ) ) ;
#9251=CARTESIAN_POINT ( 'NONE',  ( -49.99999999999999289, 515.4878487013597805, -546.7230258972048205 ) ) ;
#9262=CARTESIAN_POINT ( 'NONE',  ( -55.99999999999989342, 523.2161522479893847, -590.5524132976893270 ) ) ;
#9265=EDGE_LOOP ( 'NONE', ( #12083, #6831 ) ) ;
#9271=DIRECTION ( 'NONE',  ( 0.000000000000000000, 0.000000000000000000, -1.000000000000000000 ) ) ;
#9274=EDGE_CURVE ( 'NONE', #5350, #9290, #2197, .T. ) ;
#9277=VERTEX_POINT ( 'NONE', #389 ) ;
#9290=VERTEX_POINT ( 'NONE', #14553 ) ;
#9292=ORIENTED_EDGE ( 'NONE', *, *, #15166, .F. ) ;
#9295=EDGE_CURVE ( 'NONE', #5350, #11430, #10161, .T. ) ;
#9298=ORIENTED_EDGE ( 'NONE', *, *, #4262, .T. ) ;
#9306=AXIS2_PLACEMENT_3D ( 'NONE', #6385, #7598, #11395 ) ;
#9339=CARTESIAN_POINT ( 'NONE',  ( 46.99999999999988631, 549.5810598491746077, -518.1154249974242703 ) ) ;
#9348=CYLINDRICAL_SURFACE ( 'NONE', #2645, 59.99999999999994316 ) ;
#9352=ORIENTED_EDGE ( 'NONE', *, *, #10313, .T. ) ;
#9354=EDGE_CURVE ( 'NONE', #8101, #6054, #4128, .T. ) ;
#9355=CARTESIAN_POINT ( 'NONE',  ( 55.99999999999989342, 493.2350855268092573, -585.2659423243250103 ) ) ;
#9362=AXIS2_PLACEMENT_3D ( 'NONE', #12245, #13537, #4512 ) ;
#9368=EDGE_LOOP ( 'NONE', ( #13098, #9146, #2041, #6860 ) ) ;
#9380=VERTEX_POINT ( 'NONE', #9111 ) ;
#9390=EDGE_CURVE ( 'NONE', #3466, #8101, #2753, .T. ) ;
#9403=DIRECTION ( 'NONE',  ( -1.000000000000000000, 0.000000000000000000, -0.000000000000000000 ) ) ;
#9409=AXIS2_PLACEMENT_3D ( 'NONE', #1963, #773, #852 ) ;
#9421=CARTESIAN_POINT ( 'NONE',  ( -55.99999999999989342, 493.2350855268092573, -585.2659423243250103 ) ) ;
#9423=VERTEX_POINT ( 'NONE', #6 ) ;
#9424=CARTESIAN_POINT ( 'NONE',  ( 46.99999999999988631, 493.2350855268092573, -580.5705369404290650 ) ) ;
#9425=VECTOR ( 'NONE', #3306, 1000.000000000000114 ) ;
#9432=DIRECTION ( 'NONE',  ( 0.000000000000000000, 0.000000000000000000, 1.000000000000000000 ) ) ;
#9443=DIRECTION ( 'NONE',  ( -1.000000000000000000, 0.000000000000000000, -0.000000000000000000 ) ) ;
#9445=ORIENTED_EDGE ( 'NONE', *, *, #3427, .T. ) ;
#9451=CARTESIAN_POINT ( 'NONE',  ( 46.99999999999988631, 493.2350855268086320, -494.4847040861889127 ) ) ;
#9457=CARTESIAN_POINT ( 'NONE',  ( 55.99999999999989342, 523.2161522479893847, -576.8570079137933817 ) ) ;
#9475=ORIENTED_EDGE ( 'NONE', *, *, #6507, .T. ) ;
#9477=CARTESIAN_POINT ( 'NONE',  ( -55.99999999999989342, 493.2350855268086320, -503.4847040861888559 ) ) ;
#9481=CARTESIAN_POINT ( 'NONE',  ( 54.99999999999999289, 515.4878487013597805, -546.7230258972048205 ) ) ;
#9482=ORIENTED_EDGE ( 'NONE', *, *, #6489, .F. ) ;
#9483=CARTESIAN_POINT ( 'NONE',  ( -45.00000000000000000, 473.6663340069157471, -531.5012393965008641 ) ) ;
#9491=ORIENTED_EDGE ( 'NONE', *, *, #8132, .T. ) ;
#9494=TOROIDAL_SURFACE ( 'NONE', #14428, 4.695405383895982609, 9.000000000000000000 ) ;
#9503=VECTOR ( 'NONE', #12037, 1000.000000000000114 ) ;
#9511=CARTESIAN_POINT ( 'NONE',  ( -45.00000000000000000, 515.4878487013597805, -486.7230258972047636 ) ) ;
#9516=EDGE_CURVE ( 'NONE', #12617, #16287, #12104, .T. ) ;
#9533=DIRECTION ( 'NONE',  ( 0.000000000000000000, 0.000000000000000000, -1.000000000000000000 ) ) ;
#9537=EDGE_CURVE ( 'NONE', #5722, #1188, #9905, .T. ) ;
#9547=CARTESIAN_POINT ( 'NONE',  ( 55.99999999999989342, 473.6663340069157471, -536.1966447803968094 ) ) ;
#9571=CARTESIAN_POINT ( 'NONE',  ( -45.00000000000000000, 493.2350855268092573, -585.2659423243250103 ) ) ;
#9582=EDGE_CURVE ( 'NONE', #2950, #13599, #16744, .T. ) ;
#9587=CARTESIAN_POINT ( 'NONE',  ( 45.00000000000000000, 549.5810598491749488, -561.6352214130889706 ) ) ;
#9589=ADVANCED_FACE ( 'NONE', ( #2228 ), #10176, .T. ) ;
#9597=DIRECTION ( 'NONE',  ( 0.000000000000000000, 0.000000000000000000, -1.000000000000000000 ) ) ;
#9602=FACE_OUTER_BOUND ( 'NONE', #11461, .T. ) ;
#9607=AXIS2_PLACEMENT_3D ( 'NONE', #762, #12348, #588 ) ;
#9608=EDGE_CURVE ( 'NONE', #11869, #2250, #14011, .T. ) ;
#9609=DIRECTION ( 'NONE',  ( -1.000000000000000000, 0.000000000000000000, 0.000000000000000000 ) ) ;
#9611=EDGE_CURVE ( 'NONE', #11869, #9122, #4680, .T. ) ;
#9616=VERTEX_POINT ( 'NONE', #14673 ) ;
#9618=AXIS2_PLACEMENT_3D ( 'NONE', #2957, #13270, #1667 ) ;
#9622=EDGE_LOOP ( 'NONE', ( #7311, #16849, #16839, #7786 ) ) ;
#9637=ADVANCED_FACE ( 'NONE', ( #327 ), #7086, .T. ) ;
#9641=ORIENTED_EDGE ( 'NONE', *, *, #6851, .T. ) ;
#9645=ORIENTED_EDGE ( 'NONE', *, *, #14679, .T. ) ;
#9660=TOROIDAL_SURFACE ( 'NONE', #5804, 4.695405383895982609, 9.000000000000000000 ) ;
#9666=CIRCLE ( 'NONE', #3343, 187.4999999999998863 ) ;
#9667=EDGE_LOOP ( 'NONE', ( #11214, #6340 ) ) ;
#9671=PLANE ( 'NONE',  #3338 ) ;
#9674=LINE ( 'NONE', #14904, #12298 ) ;
#9679=CARTESIAN_POINT ( 'NONE',  ( -55.99999999999988631, 645.2345343053611941, -411.3640676610526157 ) ) ;
#9686=VERTEX_POINT ( 'NONE', #13717 ) ;
#9689=PRODUCT_DEFINITION ( 'UNKNOWN', '', #4238, #3096 ) ;
#9697=ORIENTED_EDGE ( 'NONE', *, *, #13215, .T. ) ;
#9698=DIRECTION ( 'NONE',  ( -1.000000000000000000, 0.000000000000000000, 0.000000000000000000 ) ) ;
#9704=FACE_OUTER_BOUND ( 'NONE', #7694, .T. ) ;
#9708=AXIS2_PLACEMENT_3D ( 'NONE', #1215, #1045, #4978 ) ;
#9734=ORIENTED_EDGE ( 'NONE', *, *, #3318, .T. ) ;
#9738=EDGE_CURVE ( 'NONE', #6153, #12411, #6043, .T. ) ;
#9742=DIRECTION ( 'NONE',  ( -1.000000000000000000, -0.000000000000000000, 0.000000000000000000 ) ) ;
#9767=DIRECTION ( 'NONE',  ( 1.000000000000000000, 0.000000000000000000, 0.000000000000000000 ) ) ;
#9769=CARTESIAN_POINT ( 'NONE',  ( -46.99999999999988631, 549.5810598491749488, -570.6352214130889706 ) ) ;
#9777=CYLINDRICAL_SURFACE ( 'NONE', #3886, 13.69540538389601991 ) ;
#9778=DIRECTION ( 'NONE',  ( 1.000000000000000000, -0.000000000000000000, -0.000000000000000000 ) ) ;
#9793=CIRCLE ( 'NONE', #10053, 84.99999999999997158 ) ;
#9794=DIRECTION ( 'NONE',  ( -1.000000000000000000, -0.000000000000000000, 0.000000000000000000 ) ) ;
#9796=ORIENTED_EDGE ( 'NONE', *, *, #16445, .T. ) ;
#9804=EDGE_CURVE ( 'NONE', #14998, #1375, #10184, .T. ) ;
#9810=ORIENTED_EDGE ( 'NONE', *, *, #16955, .F. ) ;
#9816=DIRECTION ( 'NONE',  ( 0.000000000000000000, 0.000000000000000000, -1.000000000000000000 ) ) ;
#9822=ORIENTED_EDGE ( 'NONE', *, *, #10235, .F. ) ;
#9831=ORIENTED_EDGE ( 'NONE', *, *, #6866, .T. ) ;
#9833=CARTESIAN_POINT ( 'NONE',  ( -55.99999999999989342, 493.2350855268086320, -494.4847040861889127 ) ) ;
#9843=DIRECTION ( 'NONE',  ( 0.000000000000000000, 0.000000000000000000, -1.000000000000000000 ) ) ;
#9844=DIRECTION ( 'NONE',  ( 1.000000000000000000, 0.000000000000000000, 0.000000000000000000 ) ) ;
#9850=ORIENTED_EDGE ( 'NONE', *, *, #9804, .F. ) ;
#9851=EDGE_LOOP ( 'NONE', ( #8295, #15371, #8611, #3980 ) ) ;
#9855=DIRECTION ( 'NONE',  ( 1.000000000000000000, -0.000000000000000000, -0.000000000000000000 ) ) ;
#9870=ORIENTED_EDGE ( 'NONE', *, *, #5097, .T. ) ;
#9879=DIRECTION ( 'NONE',  ( 0.000000000000000000, 0.000000000000000000, -1.000000000000000000 ) ) ;
#9891=DIRECTION ( 'NONE',  ( 0.000000000000000000, 0.000000000000000000, -1.000000000000000000 ) ) ;
#9892=ORIENTED_EDGE ( 'NONE', *, *, #14433, .T. ) ;
#9895=ADVANCED_FACE ( 'NONE', ( #8563 ), #14561, .T. ) ;
#9904=ORIENTED_EDGE ( 'NONE', *, *, #5097, .F. ) ;
#9905=CIRCLE ( 'NONE', #15384, 13.69540538389601991 ) ;
#9909=DIRECTION ( 'NONE',  ( 1.000000000000000000, 0.000000000000000000, -0.000000000000000000 ) ) ;
#9910=DIRECTION ( 'NONE',  ( 0.000000000000000000, 1.000000000000000000, 1.224646799147353207E-16 ) ) ;
#9929=EDGE_CURVE ( 'NONE', #14215, #3627, #6065, .T. ) ;
#9935=CARTESIAN_POINT ( 'NONE',  ( -55.99999999999989342, 559.9933750504617365, -533.0276205133087615 ) ) ;
#9945=ORIENTED_EDGE ( 'NONE', *, *, #3943, .T. ) ;
#9953=CARTESIAN_POINT ( 'NONE',  ( 175.0000000000000568, 515.4878487013597805, -546.7230258972048205 ) ) ;
#9960=DIRECTION ( 'NONE',  ( 0.000000000000000000, 0.000000000000000000, -1.000000000000000000 ) ) ;
#9961=LINE ( 'NONE', #12612, #460 ) ;
#9965=CIRCLE ( 'NONE', #7472, 4.695405383896011919 ) ;
#9967=CARTESIAN_POINT ( 'NONE',  ( -46.99999999999988631, 559.9933750504617365, -560.4184312811007658 ) ) ;
#9970=CARTESIAN_POINT ( 'NONE',  ( -45.00000000000000000, 515.4878487013597805, -546.7230258972048205 ) ) ;
#9992=AXIS2_PLACEMENT_3D ( 'NONE', #3031, #5424, #4330 ) ;
#9995=VECTOR ( 'NONE', #7078, 1000.000000000000000 ) ;
#9997=AXIS2_PLACEMENT_3D ( 'NONE', #14864, #3351, #8758 ) ;
#10004=AXIS2_PLACEMENT_3D ( 'NONE', #4561, #8766, #15213 ) ;
#10009=FACE_BOUND ( 'NONE', #6370, .T. ) ;
#10019=AXIS2_PLACEMENT_3D ( 'NONE', #9953, #2123, #769 ) ;
#10020=EDGE_LOOP ( 'NONE', ( #1214, #13618, #8842, #12888 ) ) ;
#10021=DIRECTION ( 'NONE',  ( 0.000000000000000000, 0.000000000000000000, -1.000000000000000000 ) ) ;
#10023=CYLINDRICAL_SURFACE ( 'NONE', #2007, 84.99999999999997158 ) ;
#10027=DIRECTION ( 'NONE',  ( 0.000000000000000000, 0.000000000000000000, 1.000000000000000000 ) ) ;
#10029=ADVANCED_FACE ( 'NONE', ( #2440 ), #7975, .T. ) ;
#10031=CIRCLE ( 'NONE', #8925, 9.000000000000007105 ) ;
#10033=CARTESIAN_POINT ( 'NONE',  ( -45.00000000000000000, 523.2161522479893847, -590.5524132976893270 ) ) ;
#10039=CYLINDRICAL_SURFACE ( 'NONE', #10019, 25.00000000000002132 ) ;
#10040=EDGE_CURVE ( 'NONE', #14998, #963, #3055, .T. ) ;
#10053=AXIS2_PLACEMENT_3D ( 'NONE', #697, #855, #8756 ) ;
#10055=CARTESIAN_POINT ( 'NONE',  ( -55.99999999999989342, 549.5810598491749488, -589.0260321808809749 ) ) ;
#10058=EDGE_CURVE ( 'NONE', #544, #15036, #12648, .T. ) ;
#10066=AXIS2_PLACEMENT_3D ( 'NONE', #7962, #1618, #1797 ) ;
#10081=EDGE_LOOP ( 'NONE', ( #15897, #7772 ) ) ;
#10091=PLANE ( 'NONE',  #11866 ) ;
#10098=AXIS2_PLACEMENT_3D ( 'NONE', #3423, #11150, #15351 ) ;
#10104=FACE_OUTER_BOUND ( 'NONE', #3028, .T. ) ;
#10108=DIRECTION ( 'NONE',  ( 1.000000000000000000, 0.000000000000000000, 0.000000000000000000 ) ) ;
#10119=ADVANCED_FACE ( 'NONE', ( #1771 ), #12158, .T. ) ;
#10120=FACE_OUTER_BOUND ( 'NONE', #16088, .T. ) ;
#10126=CARTESIAN_POINT ( 'NONE',  ( -55.99999999999989342, 549.5810598491749488, -575.3306267969850296 ) ) ;
#10145=ADVANCED_FACE ( 'NONE', ( #11987 ), #9671, .T. ) ;
#10147=ADVANCED_FACE ( 'NONE', ( #10691 ), #15924, .T. ) ;
#10150=DIRECTION ( 'NONE',  ( 1.000000000000000000, -0.000000000000000000, 0.000000000000000000 ) ) ;
#10158=VECTOR ( 'NONE', #4962, 1000.000000000000000 ) ;
#10161=CIRCLE ( 'NONE', #15635, 9.000000000000007105 ) ;
#10163=CIRCLE ( 'NONE', #14004, 4.695405383896011919 ) ;
#10176=TOROIDAL_SURFACE ( 'NONE', #13747, 4.695405383895982609, 9.000000000000000000 ) ;
#10178=ORIENTED_EDGE ( 'NONE', *, *, #6249, .F. ) ;
#10184=LINE ( 'NONE', #13798, #6872 ) ;
#10187=EDGE_LOOP ( 'NONE', ( #9945, #1050, #16309, #6543 ) ) ;
#10192=FACE_OUTER_BOUND ( 'NONE', #3309, .T. ) ;
#10195=CYLINDRICAL_SURFACE ( 'NONE', #12944, 13.69540538389601991 ) ;
#10198=EDGE_LOOP ( 'NONE', ( #2100, #6187, #8571, #7115 ) ) ;
#10219=EDGE_LOOP ( 'NONE', ( #12317, #8081, #7357, #9029 ) ) ;
#10230=ORIENTED_EDGE ( 'NONE', *, *, #16926, .T. ) ;
#10233=ORIENTED_EDGE ( 'NONE', *, *, #4582, .T. ) ;
#10235=EDGE_CURVE ( 'NONE', #2243, #14813, #36, .T. ) ;
#10236=CARTESIAN_POINT ( 'NONE',  ( -55.99999999999989342, 493.2350855268092573, -585.2659423243250103 ) ) ;
#10240=CIRCLE ( 'NONE', #1186, 13.69540538389597017 ) ;
#10265=DIRECTION ( 'NONE',  ( 0.000000000000000000, 0.000000000000000000, 1.000000000000000000 ) ) ;
#10266=CIRCLE ( 'NONE', #4505, 13.69540538389601991 ) ;
#10269=EDGE_LOOP ( 'NONE', ( #6262, #10993, #888, #6140 ) ) ;
#10279=VECTOR ( 'NONE', #617, 1000.000000000000000 ) ;
#10283=PRODUCT ( 'Part6', 'Part6', '', ( #3025 ) ) ;
#10289=DIRECTION ( 'NONE',  ( 0.000000000000000000, -0.6427876096865404731, 0.7660444431189771253 ) ) ;
#10296=FACE_OUTER_BOUND ( 'NONE', #14074, .T. ) ;
#10305=CARTESIAN_POINT ( 'NONE',  ( -55.99999999999989342, 549.5810598491749488, -575.3306267969850296 ) ) ;
#10310=DIRECTION ( 'NONE',  ( -1.000000000000000000, -0.000000000000000000, 0.000000000000000000 ) ) ;
#10311=AXIS2_PLACEMENT_3D ( 'NONE', #6776, #8073, #15970 ) ;
#10313=EDGE_CURVE ( 'NONE', #12863, #9277, #13218, .T. ) ;
#10319=AXIS2_PLACEMENT_3D ( 'NONE', #11571, #7785, #16805 ) ;
#10320=CARTESIAN_POINT ( 'NONE',  ( 45.00000000000000000, 493.2350855268086320, -508.1801094700848580 ) ) ;
#10321=DIRECTION ( 'NONE',  ( 0.000000000000000000, 0.6427876096865285938, 0.7660444431189872283 ) ) ;
#10322=EDGE_LOOP ( 'NONE', ( #6729, #13561 ) ) ;
#10326=ORIENTED_EDGE ( 'NONE', *, *, #9274, .F. ) ;
#10330=AXIS2_PLACEMENT_3D ( 'NONE', #6927, #9609, #10715 ) ;
#10345=ADVANCED_FACE ( 'NONE', ( #6613 ), #15570, .T. ) ;
#10361=ORIENTED_EDGE ( 'NONE', *, *, #13173, .T. ) ;
#10364=ADVANCED_FACE ( 'NONE', ( #7735 ), #9660, .T. ) ;
#10388=VERTEX_POINT ( 'NONE', #118 ) ;
#10389=DIRECTION ( 'NONE',  ( 0.000000000000000000, 0.000000000000000000, -1.000000000000000000 ) ) ;
#10406=CARTESIAN_POINT ( 'NONE',  ( 55.99999999999989342, 523.2161522479888163, -502.8936384967199729 ) ) ;
#10408=ORIENTED_EDGE ( 'NONE', *, *, #16315, .T. ) ;
#10412=CYLINDRICAL_SURFACE ( 'NONE', #2229, 13.69540538389601991 ) ;
#10413=DIRECTION ( 'NONE',  ( -1.000000000000000000, -0.000000000000000000, 0.000000000000000000 ) ) ;
#10415=ORIENTED_EDGE ( 'NONE', *, *, #1208, .F. ) ;
#10417=CARTESIAN_POINT ( 'NONE',  ( 46.99999999999988631, 473.6663340069157471, -531.5012393965008641 ) ) ;
#10422=EDGE_LOOP ( 'NONE', ( #14786, #3603, #16174, #4717 ) ) ;
#10423=ADVANCED_FACE ( 'NONE', ( #13164 ), #10412, .T. ) ;
#10428=AXIS2_PLACEMENT_3D ( 'NONE', #6059, #7346, #8741 ) ;
#10431=ORIENTED_EDGE ( 'NONE', *, *, #4967, .T. ) ;
#10435=ORIENTED_EDGE ( 'NONE', *, *, #7298, .F. ) ;
#10439=CARTESIAN_POINT ( 'NONE',  ( -55.99999999999988631, 515.4878487013597805, -546.7230258972048205 ) ) ;
#10440=FACE_OUTER_BOUND ( 'NONE', #4139, .T. ) ;
#10443=CARTESIAN_POINT ( 'NONE',  ( -55.99999999999989342, 473.6663340069157471, -531.5012393965008641 ) ) ;
#10448=DIRECTION ( 'NONE',  ( 0.000000000000000000, 1.000000000000000000, 1.224646799147353207E-16 ) ) ;
#10453=PLANE ( 'NONE',  #13500 ) ;
#10457=ORIENTED_EDGE ( 'NONE', *, *, #11377, .F. ) ;
#10462=CARTESIAN_POINT ( 'NONE',  ( 45.00000000000000000, 515.4878487013597805, -546.7230258972048205 ) ) ;
#10467=DIRECTION ( 'NONE',  ( 0.000000000000000000, 1.000000000000000000, 1.224646799147353207E-16 ) ) ;
#10469=FACE_OUTER_BOUND ( 'NONE', #1401, .T. ) ;
#10473=CARTESIAN_POINT ( 'NONE',  ( 45.00000000000000000, 473.6663340069157471, -545.1966447803968094 ) ) ;
#10474=AXIS2_PLACEMENT_3D ( 'NONE', #4043, #2924, #6691 ) ;
#10477=DIRECTION ( 'NONE',  ( 0.000000000000000000, 0.000000000000000000, -1.000000000000000000 ) ) ;
#10480=FACE_OUTER_BOUND ( 'NONE', #136, .T. ) ;
#10483=DIRECTION ( 'NONE',  ( 0.000000000000000000, 0.000000000000000000, -1.000000000000000000 ) ) ;
#10485=EDGE_LOOP ( 'NONE', ( #12211, #4796, #2552, #6300 ) ) ;
#10486=DIRECTION ( 'NONE',  ( 0.000000000000000000, 0.000000000000000000, 1.000000000000000000 ) ) ;
#10504=FACE_BOUND ( 'NONE', #15252, .T. ) ;
#10507=CARTESIAN_POINT ( 'NONE',  ( 55.99999999999989342, 473.6663340069158039, -561.9448123979092315 ) ) ;
#10523=CARTESIAN_POINT ( 'NONE',  ( -55.99999999999989342, 493.2350855268092573, -598.9613477082210693 ) ) ;
#10527=CARTESIAN_POINT ( 'NONE',  ( 46.99999999999988631, 549.5810598491749488, -575.3306267969850296 ) ) ;
#10531=EDGE_CURVE ( 'NONE', #12736, #6401, #13516, .T. ) ;
#10547=PLANE ( 'NONE',  #8946 ) ;
#10559=DIRECTION ( 'NONE',  ( 0.000000000000000000, 0.000000000000000000, 1.000000000000000000 ) ) ;
#10565=CARTESIAN_POINT ( 'NONE',  ( 46.99999999999988631, 523.2161522479888163, -507.5890438806159750 ) ) ;
#10566=CARTESIAN_POINT ( 'NONE',  ( 46.99999999999988631, 473.6663340069158039, -561.9448123979092315 ) ) ;
#10571=CARTESIAN_POINT ( 'NONE',  ( 46.99999999999988631, 559.9933750504617365, -546.7230258972048205 ) ) ;
#10580=EDGE_LOOP ( 'NONE', ( #479, #13268 ) ) ;
#10585=CIRCLE ( 'NONE', #3192, 4.695405383896011919 ) ;
#10586=ORIENTED_EDGE ( 'NONE', *, *, #3922, .F. ) ;
#10587=AXIS2_PLACEMENT_3D ( 'NONE', #220, #1244, #1327 ) ;
#10596=DIRECTION ( 'NONE',  ( 1.000000000000000000, 0.000000000000000000, 0.000000000000000000 ) ) ;
#10603=FACE_BOUND ( 'NONE', #1484, .T. ) ;
#10616=DIRECTION ( 'NONE',  ( -1.000000000000000000, -0.000000000000000000, -0.000000000000000000 ) ) ;
#10617=CARTESIAN_POINT ( 'NONE',  ( 46.99999999999988631, 473.6663340069158039, -561.9448123979092315 ) ) ;
#10623=DIRECTION ( 'NONE',  ( 0.000000000000000000, 0.000000000000000000, 1.000000000000000000 ) ) ;
#10640=CARTESIAN_POINT ( 'NONE',  ( -46.99999999999988631, 473.6663340069158039, -561.9448123979092315 ) ) ;
#10642=DIRECTION ( 'NONE',  ( 1.000000000000000000, 0.000000000000000000, 0.000000000000000000 ) ) ;
#10645=ADVANCED_FACE ( 'NONE', ( #4816 ), #3283, .T. ) ;
#10652=CARTESIAN_POINT ( 'NONE',  ( 45.00000000000000000, 559.9933750504617365, -546.7230258972048205 ) ) ;
#10657=ORIENTED_EDGE ( 'NONE', *, *, #7206, .F. ) ;
#10658=EDGE_LOOP ( 'NONE', ( #12033, #9025 ) ) ;
#10660=EDGE_CURVE ( 'NONE', #3412, #614, #11559, .T. ) ;
#10669=EDGE_CURVE ( 'NONE', #15569, #4216, #794, .T. ) ;
#10674=DIRECTION ( 'NONE',  ( -1.000000000000000000, -0.000000000000000000, -0.000000000000000000 ) ) ;
#10678=ORIENTED_EDGE ( 'NONE', *, *, #13174, .T. ) ;
#10679=DIRECTION ( 'NONE',  ( 0.000000000000000000, 0.000000000000000000, -1.000000000000000000 ) ) ;
#10680=LINE ( 'NONE', #5251, #1739 ) ;
#10691=FACE_OUTER_BOUND ( 'NONE', #10187, .T. ) ;
#10693=ORIENTED_EDGE ( 'NONE', *, *, #13389, .F. ) ;
#10694=LINE ( 'NONE', #10523, #12395 ) ;
#10697=CARTESIAN_POINT ( 'NONE',  ( -45.00000000000000000, 515.4878487013597805, -546.7230258972048205 ) ) ;
#10706=FACE_OUTER_BOUND ( 'NONE', #6241, .T. ) ;
#10711=DIRECTION ( 'NONE',  ( 0.000000000000000000, 1.000000000000000000, -1.224646799147353207E-16 ) ) ;
#10713=VERTEX_POINT ( 'NONE', #6009 ) ;
#10715=DIRECTION ( 'NONE',  ( 0.000000000000000000, 0.000000000000000000, 1.000000000000000000 ) ) ;
#10718=DIRECTION ( 'NONE',  ( 1.000000000000000000, -0.000000000000000000, 0.000000000000000000 ) ) ;
#10720=ORIENTED_EDGE ( 'NONE', *, *, #13174, .F. ) ;
#10721=DIRECTION ( 'NONE',  ( -1.000000000000000000, -0.000000000000000000, -0.000000000000000000 ) ) ;
#10724=DIRECTION ( 'NONE',  ( -1.000000000000000000, -0.000000000000000000, -0.000000000000000000 ) ) ;
#10725=CARTESIAN_POINT ( 'NONE',  ( -46.99999999999988631, 523.2161522479893847, -590.5524132976893270 ) ) ;
#10727=CARTESIAN_POINT ( 'NONE',  ( -55.99999999999988631, 460.1944820612779381, -191.6957561970704660 ) ) ;
#10730=EDGE_CURVE ( 'NONE', #4486, #7744, #16250, .T. ) ;
#10733=DIRECTION ( 'NONE',  ( 0.000000000000000000, 0.000000000000000000, -1.000000000000000000 ) ) ;
#10735=CARTESIAN_POINT ( 'NONE',  ( 46.99999999999988631, 549.5810598491746077, -518.1154249974242703 ) ) ;
#10739=AXIS2_PLACEMENT_3D ( 'NONE', #5196, #14067, #9173 ) ;
#10743=CARTESIAN_POINT ( 'NONE',  ( 54.99999999999999289, 515.4878487013597805, -631.7230258972047068 ) ) ;
#10781=AXIS2_PLACEMENT_3D ( 'NONE', #14812, #2955, #2865 ) ;
#10786=EDGE_CURVE ( 'NONE', #15233, #3412, #14436, .T. ) ;
#10801=DIRECTION ( 'NONE',  ( 0.000000000000000000, 1.000000000000000000, -1.224646799147353207E-16 ) ) ;
#10807=ORIENTED_EDGE ( 'NONE', *, *, #14550, .T. ) ;
#10808=DIRECTION ( 'NONE',  ( 0.000000000000000000, 0.000000000000000000, 1.000000000000000000 ) ) ;
#10809=CIRCLE ( 'NONE', #3406, 13.69540538389601991 ) ;
#10816=ORIENTED_EDGE ( 'NONE', *, *, #16955, .T. ) ;
#10817=CIRCLE ( 'NONE', #9997, 13.69540538389601991 ) ;
#10822=CIRCLE ( 'NONE', #13295, 4.695405383896011919 ) ;
#10831=CARTESIAN_POINT ( 'NONE',  ( -45.00000000000000000, 549.5810598491749488, -575.3306267969850296 ) ) ;
#10834=ORIENTED_EDGE ( 'NONE', *, *, #8581, .T. ) ;
#10841=EDGE_CURVE ( 'NONE', #4299, #15837, #5817, .T. ) ;
#10843=ORIENTED_EDGE ( 'NONE', *, *, #14026, .T. ) ;
#10847=EDGE_CURVE ( 'NONE', #3545, #12955, #4183, .T. ) ;
#10848=ORIENTED_EDGE ( 'NONE', *, *, #3573, .F. ) ;
#10855=FACE_OUTER_BOUND ( 'NONE', #12607, .T. ) ;
#10868=CARTESIAN_POINT ( 'NONE',  ( -46.99999999999988631, 473.6663340069158039, -566.6402177818052905 ) ) ;
#10872=FACE_OUTER_BOUND ( 'NONE', #9667, .T. ) ;
#10873=ADVANCED_FACE ( 'NONE', ( #6853 ), #8070, .T. ) ;
#10877=AXIS2_PLACEMENT_3D ( 'NONE', #14584, #78, #8052 ) ;
#10879=DIRECTION ( 'NONE',  ( 1.000000000000000000, 0.000000000000000000, -0.000000000000000000 ) ) ;
#10880=CARTESIAN_POINT ( 'NONE',  ( -45.00000000000000000, 523.2161522479888163, -489.1982331128240276 ) ) ;
#10881=DIRECTION ( 'NONE',  ( -1.000000000000000000, -0.000000000000000000, -0.000000000000000000 ) ) ;
#10882=EDGE_LOOP ( 'NONE', ( #14852, #11285, #4630, #16336 ) ) ;
#10887=DIRECTION ( 'NONE',  ( -1.000000000000000000, -0.000000000000000000, 0.000000000000000000 ) ) ;
#10890=EDGE_CURVE ( 'NONE', #614, #3412, #4720, .T. ) ;
#10898=VERTEX_POINT ( 'NONE', #10727 ) ;
#10899=CARTESIAN_POINT ( 'NONE',  ( -46.99999999999988631, 473.6663340069157471, -531.5012393965008641 ) ) ;
#10900=DIRECTION ( 'NONE',  ( 0.000000000000000000, 0.000000000000000000, 1.000000000000000000 ) ) ;
#10902=CIRCLE ( 'NONE', #752, 13.69540538389601991 ) ;
#10905=DIRECTION ( 'NONE',  ( 0.000000000000000000, 0.000000000000000000, 1.000000000000000000 ) ) ;
#10908=CYLINDRICAL_SURFACE ( 'NONE', #11109, 13.69540538389601991 ) ;
#10914=CARTESIAN_POINT ( 'NONE',  ( -46.99999999999988631, 549.5810598491746077, -518.1154249974242703 ) ) ;
#10916=DIRECTION ( 'NONE',  ( 1.000000000000000000, 0.000000000000000000, 0.000000000000000000 ) ) ;
#10922=ORIENTED_EDGE ( 'NONE', *, *, #13916, .T. ) ;
#10923=AXIS2_PLACEMENT_3D ( 'NONE', #8576, #4617, #15188 ) ;
#10928=ORIENTED_EDGE ( 'NONE', *, *, #241, .T. ) ;
#10938=EDGE_CURVE ( 'NONE', #16590, #9423, #5546, .T. ) ;
#10940=EDGE_LOOP ( 'NONE', ( #11962, #15236 ) ) ;
#10944=ORIENTED_EDGE ( 'NONE', *, *, #10730, .T. ) ;
#10945=ADVANCED_FACE ( 'NONE', ( #15798 ), #14696, .T. ) ;
#10958=CARTESIAN_POINT ( 'NONE',  ( 45.00000000000000000, 549.5810598491749488, -575.3306267969850296 ) ) ;
#10965=AXIS2_PLACEMENT_3D ( 'NONE', #261, #10724, #14692 ) ;
#10973=ORIENTED_EDGE ( 'NONE', *, *, #1855, .T. ) ;
#10977=CARTESIAN_POINT ( 'NONE',  ( 54.99999999999999289, 515.4878487013597805, -546.7230258972048205 ) ) ;
#10979=AXIS2_PLACEMENT_3D ( 'NONE', #10305, #948, #3695 ) ;
#10983=ORIENTED_EDGE ( 'NONE', *, *, #9390, .F. ) ;
#10992=LINE ( 'NONE', #262, #6918 ) ;
#10993=ORIENTED_EDGE ( 'NONE', *, *, #11006, .T. ) ;
#10995=PRODUCT_DEFINITION_SHAPE ( 'NONE', 'NONE',  #9689 ) ;
#11001=ORIENTED_EDGE ( 'NONE', *, *, #2873, .F. ) ;
#11006=EDGE_CURVE ( 'NONE', #2782, #12863, #7440, .T. ) ;
#11016=FACE_OUTER_BOUND ( 'NONE', #8847, .T. ) ;
#11018=ORIENTED_EDGE ( 'NONE', *, *, #6044, .F. ) ;
#11030=DIRECTION ( 'NONE',  ( 0.000000000000000000, 0.000000000000000000, -1.000000000000000000 ) ) ;
#11033=AXIS2_PLACEMENT_3D ( 'NONE', #182, #8330, #1372 ) ;
#11040=EDGE_LOOP ( 'NONE', ( #14525, #13621, #6804, #6432 ) ) ;
#11046=ORIENTED_EDGE ( 'NONE', *, *, #5912, .F. ) ;
#11057=ADVANCED_FACE ( 'NONE', ( #6072 ), #6619, .T. ) ;
#11058=DIRECTION ( 'NONE',  ( 0.000000000000000000, 0.000000000000000000, -1.000000000000000000 ) ) ;
#11061=CARTESIAN_POINT ( 'NONE',  ( 46.99999999999988631, 493.2350855268086320, -508.1801094700848580 ) ) ;
#11068=CARTESIAN_POINT ( 'NONE',  ( 46.99999999999988631, 473.6663340069157471, -531.5012393965008641 ) ) ;
#11089=EDGE_LOOP ( 'NONE', ( #14027, #5009, #16946, #8190 ) ) ;
#11091=CARTESIAN_POINT ( 'NONE',  ( 54.99999999999999289, 515.4878487013597805, -359.2230258972048773 ) ) ;
#11092=CIRCLE ( 'NONE', #9164, 187.4999999999998863 ) ;
#11097=VERTEX_POINT ( 'NONE', #12610 ) ;
#11103=EDGE_LOOP ( 'NONE', ( #7836, #6519 ) ) ;
#11107=DIRECTION ( 'NONE',  ( 1.000000000000000000, 0.000000000000000000, 0.000000000000000000 ) ) ;
#11109=AXIS2_PLACEMENT_3D ( 'NONE', #8230, #6845, #177 ) ;
#11110=AXIS2_PLACEMENT_3D ( 'NONE', #4868, #6305, #3589 ) ;
#11111=ORIENTED_EDGE ( 'NONE', *, *, #16916, .T. ) ;
#11127=CARTESIAN_POINT ( 'NONE',  ( -46.99999999999988631, 523.2161522479888163, -516.5890438806160319 ) ) ;
#11129=DIRECTION ( 'NONE',  ( 0.000000000000000000, 0.000000000000000000, -1.000000000000000000 ) ) ;
#11139=VECTOR ( 'NONE', #15032, 1000.000000000000000 ) ;
#11147=DIRECTION ( 'NONE',  ( 0.000000000000000000, 0.000000000000000000, -1.000000000000000000 ) ) ;
#11150=DIRECTION ( 'NONE',  ( 0.000000000000000000, -1.000000000000000000, 0.000000000000000000 ) ) ;
#11151=ORIENTED_EDGE ( 'NONE', *, *, #4684, .F. ) ;
#11154=AXIS2_PLACEMENT_3D ( 'NONE', #164, #2813, #5465 ) ;
#11160=ORIENTED_EDGE ( 'NONE', *, *, #12244, .T. ) ;
#11162=CIRCLE ( 'NONE', #14466, 13.69540538389598083 ) ;
#11164=VERTEX_POINT ( 'NONE', #11661 ) ;
#11173=FACE_OUTER_BOUND ( 'NONE', #13339, .T. ) ;
#11187=LINE ( 'NONE', #16421, #12998 ) ;
#11207=DIRECTION ( 'NONE',  ( 0.000000000000000000, 0.000000000000000000, -1.000000000000000000 ) ) ;
#11214=ORIENTED_EDGE ( 'NONE', *, *, #8787, .T. ) ;
#11227=CARTESIAN_POINT ( 'NONE',  ( 45.00000000000000000, 515.4878487013597805, -546.7230258972048205 ) ) ;
#11232=DIRECTION ( 'NONE',  ( 1.000000000000000000, 0.000000000000000000, 0.000000000000000000 ) ) ;
#11233=DIRECTION ( 'NONE',  ( 1.000000000000000000, 0.000000000000000000, 0.000000000000000000 ) ) ;
#11234=EDGE_LOOP ( 'NONE', ( #7662, #1892, #4778, #16560, #24 ) ) ;
#11236=VECTOR ( 'NONE', #10881, 1000.000000000000000 ) ;
#11241=CARTESIAN_POINT ( 'NONE',  ( -46.99999999999988631, 549.5810598491746077, -504.4200196135282113 ) ) ;
#11258=AXIS2_PLACEMENT_3D ( 'NONE', #9175, #5381, #2720 ) ;
#11265=ORIENTED_EDGE ( 'NONE', *, *, #16562, .T. ) ;
#11270=ORIENTED_EDGE ( 'NONE', *, *, #5724, .T. ) ;
#11275=DIRECTION ( 'NONE',  ( 0.000000000000000000, 0.000000000000000000, -1.000000000000000000 ) ) ;
#11284=LINE ( 'NONE', #11454, #6293 ) ;
#11285=ORIENTED_EDGE ( 'NONE', *, *, #1483, .T. ) ;
#11288=CIRCLE ( 'NONE', #7436, 4.695405383896011919 ) ;
#11295=LINE ( 'NONE', #3320, #330 ) ;
#11296=DIRECTION ( 'NONE',  ( 1.000000000000000000, -0.000000000000000000, 0.000000000000000000 ) ) ;
#11298=ORIENTED_EDGE ( 'NONE', *, *, #12426, .T. ) ;
#11300=AXIS2_PLACEMENT_3D ( 'NONE', #6387, #9163, #10289 ) ;
#11302=EDGE_CURVE ( 'NONE', #5839, #3545, #6631, .T. ) ;
#11315=CIRCLE ( 'NONE', #6354, 9.000000000000007105 ) ;
#11320=VERTEX_POINT ( 'NONE', #13391 ) ;
#11329=VERTEX_POINT ( 'NONE', #1696 ) ;
#11330=DIRECTION ( 'NONE',  ( 0.000000000000000000, 0.000000000000000000, 1.000000000000000000 ) ) ;
#11351=FACE_OUTER_BOUND ( 'NONE', #2936, .T. ) ;
#11376=EDGE_CURVE ( 'NONE', #11430, #6541, #14061, .T. ) ;
#11377=EDGE_CURVE ( 'NONE', #13903, #7626, #14612, .T. ) ;
#11382=CIRCLE ( 'NONE', #14948, 187.4999999999998863 ) ;
#11387=EDGE_CURVE ( 'NONE', #2250, #6264, #8851, .T. ) ;
#11389=DIRECTION ( 'NONE',  ( -1.000000000000000000, 0.000000000000000000, 0.000000000000000000 ) ) ;
#11394=ORIENTED_EDGE ( 'NONE', *, *, #10660, .F. ) ;
#11395=DIRECTION ( 'NONE',  ( 0.000000000000000000, 0.000000000000000000, -1.000000000000000000 ) ) ;
#11396=AXIS2_PLACEMENT_3D ( 'NONE', #16119, #15079, #13713 ) ;
#11404=EDGE_CURVE ( 'NONE', #15749, #5980, #1443, .T. ) ;
#11411=CARTESIAN_POINT ( 'NONE',  ( -55.99999999999989342, 493.2350855268092573, -585.2659423243250103 ) ) ;
#11416=CYLINDRICAL_SURFACE ( 'NONE', #7777, 13.69540538389601991 ) ;
#11418=DIRECTION ( 'NONE',  ( -1.000000000000000000, 0.000000000000000000, -0.000000000000000000 ) ) ;
#11420=CIRCLE ( 'NONE', #5662, 9.000000000000007105 ) ;
#11430=VERTEX_POINT ( 'NONE', #13866 ) ;
#11432=DIRECTION ( 'NONE',  ( 0.000000000000000000, -1.000000000000000000, 0.000000000000000000 ) ) ;
#11440=ORIENTED_EDGE ( 'NONE', *, *, #3019, .F. ) ;
#11445=ORIENTED_EDGE ( 'NONE', *, *, #2028, .T. ) ;
#11453=DIRECTION ( 'NONE',  ( -1.000000000000000000, -0.000000000000000000, -0.000000000000000000 ) ) ;
#11454=CARTESIAN_POINT ( 'NONE',  ( -55.99999999999989342, 473.6663340069157471, -517.8058340126048051 ) ) ;
#11458=EDGE_LOOP ( 'NONE', ( #5618, #2299, #12133, #12895 ) ) ;
#11460=ORIENTED_EDGE ( 'NONE', *, *, #7829, .F. ) ;
#11461=EDGE_LOOP ( 'NONE', ( #6020, #7159, #15255, #14634 ) ) ;
#11465=DIRECTION ( 'NONE',  ( 0.000000000000000000, 0.000000000000000000, 1.000000000000000000 ) ) ;
#11468=ADVANCED_FACE ( 'NONE', ( #9602 ), #15241, .T. ) ;
#11469=DIRECTION ( 'NONE',  ( 0.000000000000000000, 0.000000000000000000, 1.000000000000000000 ) ) ;
#11471=ORIENTED_EDGE ( 'NONE', *, *, #14022, .F. ) ;
#11473=AXIS2_PLACEMENT_3D ( 'NONE', #10462, #6906, #15931 ) ;
#11475=FACE_BOUND ( 'NONE', #3997, .T. ) ;
#11481=ORIENTED_EDGE ( 'NONE', *, *, #4458, .F. ) ;
#11483=CYLINDRICAL_SURFACE ( 'NONE', #10739, 13.69540538389601991 ) ;
#11494=CARTESIAN_POINT ( 'NONE',  ( 55.99999999999989342, 559.9933750504617365, -546.7230258972048205 ) ) ;
#11500=DIRECTION ( 'NONE',  ( 1.000000000000000000, -0.000000000000000000, -0.000000000000000000 ) ) ;
#11504=AXIS2_PLACEMENT_3D ( 'NONE', #12361, #601, #13737 ) ;
#11510=ORIENTED_EDGE ( 'NONE', *, *, #6493, .T. ) ;
#11516=AXIS2_PLACEMENT_3D ( 'NONE', #10439, #6473, #9161 ) ;
#11521=CARTESIAN_POINT ( 'NONE',  ( 46.99999999999988631, 473.6663340069158039, -575.6402177818052905 ) ) ;
#11529=DIRECTION ( 'NONE',  ( 1.000000000000000000, -0.000000000000000000, -0.000000000000000000 ) ) ;
#11551=CYLINDRICAL_SURFACE ( 'NONE', #11516, 187.4999999999998863 ) ;
#11553=AXIS2_PLACEMENT_3D ( 'NONE', #4099, #12003, #8212 ) ;
#11559=CIRCLE ( 'NONE', #6331, 59.99999999999994316 ) ;
#11562=CIRCLE ( 'NONE', #7715, 13.69540538389601991 ) ;
#11563=DIRECTION ( 'NONE',  ( 0.000000000000000000, 0.000000000000000000, 1.000000000000000000 ) ) ;
#11570=AXIS2_PLACEMENT_3D ( 'NONE', #15382, #13065, #6178 ) ;
#11571=CARTESIAN_POINT ( 'NONE',  ( -46.99999999999988631, 473.6663340069157471, -531.5012393965008641 ) ) ;
#11574=DIRECTION ( 'NONE',  ( -1.000000000000000000, 0.000000000000000000, 0.000000000000000000 ) ) ;
#11586=EDGE_CURVE ( 'NONE', #750, #6348, #4068, .T. ) ;
#11588=EDGE_CURVE ( 'NONE', #16590, #13450, #5013, .T. ) ;
#11599=VECTOR ( 'NONE', #3890, 1000.000000000000000 ) ;
#11607=VERTEX_POINT ( 'NONE', #2685 ) ;
#11610=AXIS2_PLACEMENT_3D ( 'NONE', #10652, #10916, #8246 ) ;
#11612=EDGE_LOOP ( 'NONE', ( #13683, #9645 ) ) ;
#11618=VERTEX_POINT ( 'NONE', #3730 ) ;
#11620=CIRCLE ( 'NONE', #12448, 187.4999999999998863 ) ;
#11621=DIRECTION ( 'NONE',  ( 0.000000000000000000, -1.000000000000000000, 0.000000000000000000 ) ) ;
#11628=AXIS2_PLACEMENT_3D ( 'NONE', #9013, #6578, #16650 ) ;
#11645=DIRECTION ( 'NONE',  ( 0.000000000000000000, 0.000000000000000000, -1.000000000000000000 ) ) ;
#11651=DIRECTION ( 'NONE',  ( 0.000000000000000000, 0.000000000000000000, 1.000000000000000000 ) ) ;
#11661=CARTESIAN_POINT ( 'NONE',  ( -45.00000000000000000, 493.2350855268092573, -571.5705369404290650 ) ) ;
#11692=ORIENTED_EDGE ( 'NONE', *, *, #7392, .F. ) ;
#11693=ORIENTED_EDGE ( 'NONE', *, *, #11825, .T. ) ;
#11714=ORIENTED_EDGE ( 'NONE', *, *, #11302, .T. ) ;
#11723=ORIENTED_EDGE ( 'NONE', *, *, #4967, .F. ) ;
#11725=DIRECTION ( 'NONE',  ( -1.000000000000000000, -0.000000000000000000, 0.000000000000000000 ) ) ;
#11728=CARTESIAN_POINT ( 'NONE',  ( 54.99999999999999289, 515.4878487013597805, -546.7230258972048205 ) ) ;
#11732=DIRECTION ( 'NONE',  ( 0.000000000000000000, 0.000000000000000000, -1.000000000000000000 ) ) ;
#11738=AXIS2_PLACEMENT_3D ( 'NONE', #4350, #16107, #1596 ) ;
#11744=DIRECTION ( 'NONE',  ( -1.000000000000000000, -0.000000000000000000, -0.000000000000000000 ) ) ;
#11746=AXIS2_PLACEMENT_3D ( 'NONE', #2136, #7364, #858 ) ;
#11749=DIRECTION ( 'NONE',  ( 0.000000000000000000, 0.3420201433256759294, -0.9396926207859057634 ) ) ;
#11759=DIRECTION ( 'NONE',  ( 1.000000000000000000, 0.000000000000000000, 0.000000000000000000 ) ) ;
#11765=FACE_OUTER_BOUND ( 'NONE', #14514, .T. ) ;
#11769=DIRECTION ( 'NONE',  ( -1.000000000000000000, 0.000000000000000000, 0.000000000000000000 ) ) ;
#11772=DIRECTION ( 'NONE',  ( 0.000000000000000000, 0.000000000000000000, 1.000000000000000000 ) ) ;
#11786=AXIS2_PLACEMENT_3D ( 'NONE', #10899, #15950, #10808 ) ;
#11789=DIRECTION ( 'NONE',  ( 0.000000000000000000, 0.000000000000000000, -1.000000000000000000 ) ) ;
#11795=CARTESIAN_POINT ( 'NONE',  ( 55.99999999999989342, 523.2161522479893847, -595.2478186815853860 ) ) ;
#11797=CARTESIAN_POINT ( 'NONE',  ( 49.99999999999999289, 515.4878487013597805, -546.7230258972048205 ) ) ;
#11805=DIRECTION ( 'NONE',  ( 1.000000000000000000, -0.000000000000000000, -0.000000000000000000 ) ) ;
#11808=ADVANCED_FACE ( 'NONE', ( #11016 ), #1658, .T. ) ;
#11810=CARTESIAN_POINT ( 'NONE',  ( -45.00000000000000000, 515.4878487013597805, -606.7230258972047068 ) ) ;
#11815=CARTESIAN_POINT ( 'NONE',  ( 46.99999999999988631, 493.2350855268092573, -585.2659423243250103 ) ) ;
#11816=DIRECTION ( 'NONE',  ( -1.000000000000000000, -0.000000000000000000, -0.000000000000000000 ) ) ;
#11823=CARTESIAN_POINT ( 'NONE',  ( 54.99999999999999289, 460.1944820612779381, -191.6957561970704660 ) ) ;
#11825=EDGE_CURVE ( 'NONE', #12389, #21, #8323, .T. ) ;
#11831=LINE ( 'NONE', #15948, #16350 ) ;
#11845=CARTESIAN_POINT ( 'NONE',  ( -46.99999999999988631, 523.2161522479888163, -489.1982331128240276 ) ) ;
#11858=DIRECTION ( 'NONE',  ( 1.000000000000000000, -0.000000000000000000, 0.000000000000000000 ) ) ;
#11866=AXIS2_PLACEMENT_3D ( 'NONE', #14997, #16439, #3231 ) ;
#11869=VERTEX_POINT ( 'NONE', #293 ) ;
#11883=VECTOR ( 'NONE', #9855, 1000.000000000000000 ) ;
#11887=EDGE_LOOP ( 'NONE', ( #3042, #5395, #11111, #7671 ) ) ;
#11901=CIRCLE ( 'NONE', #16293, 13.69540538389601991 ) ;
#11906=CARTESIAN_POINT ( 'NONE',  ( 55.99999999999989342, 559.9933750504617365, -546.7230258972048205 ) ) ;
#11908=CIRCLE ( 'NONE', #8901, 13.69540538389601991 ) ;
#11917=EDGE_CURVE ( 'NONE', #14972, #748, #6953, .T. ) ;
#11918=VECTOR ( 'NONE', #3023, 1000.000000000000000 ) ;
#11931=CARTESIAN_POINT ( 'NONE',  ( 46.99999999999988631, 493.2350855268086320, -512.8755148539809170 ) ) ;
#11933=CYLINDRICAL_SURFACE ( 'NONE', #2387, 13.69540538389596485 ) ;
#11934=DIRECTION ( 'NONE',  ( 1.000000000000000000, 0.000000000000000000, 0.000000000000000000 ) ) ;
#11948=CARTESIAN_POINT ( 'NONE',  ( 55.99999999999989342, 549.5810598491749488, -589.0260321808809749 ) ) ;
#11950=DIRECTION ( 'NONE',  ( 1.000000000000000000, 0.000000000000000000, -0.000000000000000000 ) ) ;
#11959=EDGE_CURVE ( 'NONE', #1481, #10388, #12994, .T. ) ;
#11961=SHAPE_DEFINITION_REPRESENTATION ( #10995, #1883 ) ;
#11962=ORIENTED_EDGE ( 'NONE', *, *, #12164, .F. ) ;
#11969=DIRECTION ( 'NONE',  ( 0.000000000000000000, 0.000000000000000000, -1.000000000000000000 ) ) ;
#11979=AXIS2_PLACEMENT_3D ( 'NONE', #2053, #15201, #7283 ) ;
#11987=FACE_OUTER_BOUND ( 'NONE', #14138, .T. ) ;
#11988=CARTESIAN_POINT ( 'NONE',  ( -55.99999999999988631, 658.4713480608917280, -425.4301204538002139 ) ) ;
#11992=CARTESIAN_POINT ( 'NONE',  ( 55.99999999999989342, 493.2350855268086320, -512.8755148539809170 ) ) ;
#12000=ORIENTED_EDGE ( 'NONE', *, *, #4654, .F. ) ;
#12002=DIRECTION ( 'NONE',  ( 0.000000000000000000, 0.000000000000000000, 1.000000000000000000 ) ) ;
#12003=DIRECTION ( 'NONE',  ( -1.000000000000000000, -0.000000000000000000, -0.000000000000000000 ) ) ;
#12008=DIRECTION ( 'NONE',  ( 0.000000000000000000, 0.000000000000000000, 1.000000000000000000 ) ) ;
#12014=FACE_OUTER_BOUND ( 'NONE', #13677, .T. ) ;
#12015=DIRECTION ( 'NONE',  ( 1.000000000000000000, -0.000000000000000000, -0.000000000000000000 ) ) ;
#12020=ADVANCED_BREP_SHAPE_REPRESENTATION ( '', ( #14587, #1488 ), #16030 ) ;
#12022=CYLINDRICAL_SURFACE ( 'NONE', #10965, 60.00000000000000000 ) ;
#12032=PLANE ( 'NONE',  #10311 ) ;
#12033=ORIENTED_EDGE ( 'NONE', *, *, #1817, .F. ) ;
#12037=DIRECTION ( 'NONE',  ( 0.000000000000000000, -0.6930515690182840194, -0.7208880098054721852 ) ) ;
#12038=ORIENTED_EDGE ( 'NONE', *, *, #5777, .T. ) ;
#12043=CARTESIAN_POINT ( 'NONE',  ( -55.99999999999989342, 473.6663340069158039, -561.9448123979092315 ) ) ;
#12053=EDGE_CURVE ( 'NONE', #1073, #11097, #15731, .T. ) ;
#12056=AXIS2_PLACEMENT_3D ( 'NONE', #14567, #4171, #12075 ) ;
#12067=TOROIDAL_SURFACE ( 'NONE', #6273, 4.695405383895982609, 9.000000000000000000 ) ;
#12075=DIRECTION ( 'NONE',  ( 0.000000000000000000, 0.000000000000000000, 1.000000000000000000 ) ) ;
#12076=DIRECTION ( 'NONE',  ( -1.000000000000000000, -0.000000000000000000, 0.000000000000000000 ) ) ;
#12081=FACE_OUTER_BOUND ( 'NONE', #13601, .T. ) ;
#12083=ORIENTED_EDGE ( 'NONE', *, *, #6766, .F. ) ;
#12093=ORIENTED_EDGE ( 'NONE', *, *, #1208, .T. ) ;
#12096=DIRECTION ( 'NONE',  ( 0.000000000000000000, -1.000000000000000000, -0.000000000000000000 ) ) ;
#12104=CIRCLE ( 'NONE', #11258, 9.000000000000007105 ) ;
#12110=CARTESIAN_POINT ( 'NONE',  ( 49.99999999999999289, 515.4878487013597805, -546.7230258972048205 ) ) ;
#12112=AXIS2_PLACEMENT_3D ( 'NONE', #16103, #6812, #12322 ) ;
#12115=DIRECTION ( 'NONE',  ( 0.000000000000000000, 0.6427876096865285938, 0.7660444431189872283 ) ) ;
#12121=ADVANCED_FACE ( 'NONE', ( #10480 ), #7496, .T. ) ;
#12133=ORIENTED_EDGE ( 'NONE', *, *, #3362, .T. ) ;
#12135=CARTESIAN_POINT ( 'NONE',  ( -55.99999999999989342, 559.9933750504617365, -542.0276205133087615 ) ) ;
#12138=AXIS2_PLACEMENT_3D ( 'NONE', #12689, #928, #3676 ) ;
#12158=CYLINDRICAL_SURFACE ( 'NONE', #9362, 13.69540538389601991 ) ;
#12162=AXIS2_PLACEMENT_3D ( 'NONE', #7164, #11389, #2194 ) ;
#12164=EDGE_CURVE ( 'NONE', #1188, #5722, #14926, .T. ) ;
#12170=CYLINDRICAL_SURFACE ( 'NONE', #5303, 13.69540538389601991 ) ;
#12173=EDGE_LOOP ( 'NONE', ( #10843, #10807, #340, #4480 ) ) ;
#12174=AXIS2_PLACEMENT_3D ( 'NONE', #9483, #1753, #2772 ) ;
#12175=DIRECTION ( 'NONE',  ( -1.000000000000000000, 0.000000000000000000, -0.000000000000000000 ) ) ;
#12177=AXIS2_PLACEMENT_3D ( 'NONE', #8116, #5363, #14562 ) ;
#12188=CIRCLE ( 'NONE', #4241, 13.69540538389601991 ) ;
#12198=CARTESIAN_POINT ( 'NONE',  ( -55.99999999999989342, 473.6663340069158039, -557.2494070140132862 ) ) ;
#12203=AXIS2_PLACEMENT_3D ( 'NONE', #14961, #16242, #16485 ) ;
#12205=UNCERTAINTY_MEASURE_WITH_UNIT (LENGTH_MEASURE( 1.000000000000000082E-05 ), #3381, 'distance_accuracy_value', 'NONE');
#12209=CARTESIAN_POINT ( 'NONE',  ( 55.99999999999989342, 473.6663340069158039, -566.6402177818052905 ) ) ;
#12211=ORIENTED_EDGE ( 'NONE', *, *, #3072, .T. ) ;
#12214=VERTEX_POINT ( 'NONE', #9547 ) ;
#12217=VECTOR ( 'NONE', #4619, 1000.000000000000000 ) ;
#12221=ORIENTED_EDGE ( 'NONE', *, *, #13038, .F. ) ;
#12230=EDGE_CURVE ( 'NONE', #14286, #15101, #15192, .T. ) ;
#12233=ORIENTED_EDGE ( 'NONE', *, *, #1710, .T. ) ;
#12237=ORIENTED_EDGE ( 'NONE', *, *, #11586, .F. ) ;
#12244=EDGE_CURVE ( 'NONE', #13085, #15297, #14641, .T. ) ;
#12245=CARTESIAN_POINT ( 'NONE',  ( 55.99999999999989342, 473.6663340069157471, -531.5012393965008641 ) ) ;
#12252=EDGE_CURVE ( 'NONE', #1386, #3583, #2014, .T. ) ;
#12259=CYLINDRICAL_SURFACE ( 'NONE', #15465, 13.69540538389601991 ) ;
#12276=CIRCLE ( 'NONE', #8147, 25.00000000000002132 ) ;
#12278=DIRECTION ( 'NONE',  ( 0.000000000000000000, 0.000000000000000000, 1.000000000000000000 ) ) ;
#12279=ORIENTED_EDGE ( 'NONE', *, *, #7090, .F. ) ;
#12283=DIRECTION ( 'NONE',  ( 1.000000000000000000, -0.000000000000000000, -0.000000000000000000 ) ) ;
#12287=FACE_OUTER_BOUND ( 'NONE', #15390, .T. ) ;
#12296=CIRCLE ( 'NONE', #16128, 4.695405383896011919 ) ;
#12298=VECTOR ( 'NONE', #8118, 1000.000000000000000 ) ;
#12305=EDGE_LOOP ( 'NONE', ( #6327, #6515, #5332, #16130 ) ) ;
#12306=CARTESIAN_POINT ( 'NONE',  ( -46.99999999999988631, 549.5810598491746077, -513.4200196135282113 ) ) ;
#12317=ORIENTED_EDGE ( 'NONE', *, *, #3760, .T. ) ;
#12319=ADVANCED_FACE ( 'NONE', ( #13332 ), #4217, .T. ) ;
#12322=DIRECTION ( 'NONE',  ( 0.000000000000000000, 0.000000000000000000, 1.000000000000000000 ) ) ;
#12324=VECTOR ( 'NONE', #11453, 1000.000000000000000 ) ;
#12325=FACE_OUTER_BOUND ( 'NONE', #10198, .T. ) ;
#12331=EDGE_CURVE ( 'NONE', #12394, #12986, #10817, .T. ) ;
#12335=EDGE_LOOP ( 'NONE', ( #9822, #1015 ) ) ;
#12340=CARTESIAN_POINT ( 'NONE',  ( -54.99999999999999289, 515.4878487013597805, -546.7230258972048205 ) ) ;
#12342=DIRECTION ( 'NONE',  ( 0.000000000000000000, -1.000000000000000000, 0.000000000000000000 ) ) ;
#12348=DIRECTION ( 'NONE',  ( 1.000000000000000000, -0.000000000000000000, 0.000000000000000000 ) ) ;
#12356=EDGE_LOOP ( 'NONE', ( #4699, #132 ) ) ;
#12359=ADVANCED_FACE ( 'NONE', ( #7363 ), #3963, .T. ) ;
#12361=CARTESIAN_POINT ( 'NONE',  ( -55.99999999999989342, 549.5810598491749488, -575.3306267969850296 ) ) ;
#12372=LINE ( 'NONE', #4629, #13344 ) ;
#12381=AXIS2_PLACEMENT_3D ( 'NONE', #4743, #7478, #13863 ) ;
#12382=ORIENTED_EDGE ( 'NONE', *, *, #10786, .F. ) ;
#12389=VERTEX_POINT ( 'NONE', #11241 ) ;
#12394=VERTEX_POINT ( 'NONE', #699 ) ;
#12395=VECTOR ( 'NONE', #6735, 1000.000000000000000 ) ;
#12411=VERTEX_POINT ( 'NONE', #3267 ) ;
#12413=CARTESIAN_POINT ( 'NONE',  ( -45.00000000000000000, 493.2350855268092573, -585.2659423243250103 ) ) ;
#12415=FACE_OUTER_BOUND ( 'NONE', #6463, .T. ) ;
#12424=CARTESIAN_POINT ( 'NONE',  ( 55.99999999999989342, 559.9933750504617365, -542.0276205133087615 ) ) ;
#12425=ORIENTED_EDGE ( 'NONE', *, *, #2728, .F. ) ;
#12426=EDGE_CURVE ( 'NONE', #12389, #3004, #10266, .T. ) ;
#12443=DIRECTION ( 'NONE',  ( 1.000000000000000000, 0.000000000000000000, 0.000000000000000000 ) ) ;
#12448=AXIS2_PLACEMENT_3D ( 'NONE', #15490, #15571, #7831 ) ;
#12451=VERTEX_POINT ( 'NONE', #943 ) ;
#12454=ADVANCED_FACE ( 'NONE', ( #7112 ), #11416, .T. ) ;
#12455=DIRECTION ( 'NONE',  ( 1.000000000000000000, -0.000000000000000000, 0.000000000000000000 ) ) ;
#12483=VERTEX_POINT ( 'NONE', #3941 ) ;
#12489=EDGE_CURVE ( 'NONE', #6264, #9122, #8893, .T. ) ;
#12492=CARTESIAN_POINT ( 'NONE',  ( -55.99999999999989342, 473.6663340069158039, -561.9448123979092315 ) ) ;
#12497=ORIENTED_EDGE ( 'NONE', *, *, #11959, .T. ) ;
#12499=DIRECTION ( 'NONE',  ( 0.000000000000000000, -0.6468954956981580739, 0.7625786632508375629 ) ) ;
#12502=CARTESIAN_POINT ( 'NONE',  ( 54.99999999999999289, 515.4878487013597805, -631.7230258972047068 ) ) ;
#12527=FACE_OUTER_BOUND ( 'NONE', #13158, .T. ) ;
#12532=DIRECTION ( 'NONE',  ( 0.000000000000000000, 0.000000000000000000, 1.000000000000000000 ) ) ;
#12534=CARTESIAN_POINT ( 'NONE',  ( 46.99999999999988631, 549.5810598491746077, -504.4200196135282113 ) ) ;
#12536=CIRCLE ( 'NONE', #1827, 9.000000000000007105 ) ;
#12551=EDGE_CURVE ( 'NONE', #5265, #12214, #13287, .T. ) ;
#12553=ADVANCED_FACE ( 'NONE', ( #8930 ), #4881, .T. ) ;
#12560=AXIS2_PLACEMENT_3D ( 'NONE', #2121, #681, #8492 ) ;
#12566=ORIENTED_EDGE ( 'NONE', *, *, #7181, .F. ) ;
#12568=EDGE_CURVE ( 'NONE', #11607, #14915, #2468, .T. ) ;
#12572=AXIS2_PLACEMENT_3D ( 'NONE', #1923, #5791, #13371 ) ;
#12576=CARTESIAN_POINT ( 'NONE',  ( -55.99999999999989342, 473.6663340069157471, -531.5012393965008641 ) ) ;
#12578=DIRECTION ( 'NONE',  ( 0.000000000000000000, -1.000000000000000000, 0.000000000000000000 ) ) ;
#12580=EDGE_LOOP ( 'NONE', ( #15835, #12985, #9831, #5437 ) ) ;
#12585=ORIENTED_EDGE ( 'NONE', *, *, #14983, .F. ) ;
#12586=ORIENTED_EDGE ( 'NONE', *, *, #11825, .F. ) ;
#12589=CARTESIAN_POINT ( 'NONE',  ( 175.0000000000000568, 515.4878487013597805, -521.7230258972047068 ) ) ;
#12590=VERTEX_POINT ( 'NONE', #12952 ) ;
#12605=DIRECTION ( 'NONE',  ( 0.000000000000000000, 0.000000000000000000, -1.000000000000000000 ) ) ;
#12607=EDGE_LOOP ( 'NONE', ( #10720, #13505, #12843, #270 ) ) ;
#12610=CARTESIAN_POINT ( 'NONE',  ( -45.00000000000000000, 493.2350855268086320, -494.4847040861889127 ) ) ;
#12612=CARTESIAN_POINT ( 'NONE',  ( 55.99999999999989342, 559.9933750504617365, -533.0276205133087615 ) ) ;
#12616=CARTESIAN_POINT ( 'NONE',  ( 54.99999999999999289, 645.2345343053615352, -411.3640676610528999 ) ) ;
#12617=VERTEX_POINT ( 'NONE', #14327 ) ;
#12627=CIRCLE ( 'NONE', #11786, 13.69540538389601991 ) ;
#12629=CARTESIAN_POINT ( 'NONE',  ( 46.99999999999988631, 523.2161522479888163, -489.1982331128240276 ) ) ;
#12635=ORIENTED_EDGE ( 'NONE', *, *, #6107, .F. ) ;
#12644=EDGE_CURVE ( 'NONE', #4130, #12617, #12627, .T. ) ;
#12648=CIRCLE ( 'NONE', #12112, 9.000000000000007105 ) ;
#12659=FACE_BOUND ( 'NONE', #102, .T. ) ;
#12661=ORIENTED_EDGE ( 'NONE', *, *, #6875, .T. ) ;
#12664=EDGE_CURVE ( 'NONE', #14463, #750, #2464, .T. ) ;
#12665=EDGE_CURVE ( 'NONE', #4486, #11329, #8781, .T. ) ;
#12667=CIRCLE ( 'NONE', #7993, 9.000000000000007105 ) ;
#12675=DIRECTION ( 'NONE',  ( 0.000000000000000000, 1.000000000000000000, 1.224646799147353207E-16 ) ) ;
#12676=DIRECTION ( 'NONE',  ( -1.000000000000000000, -0.000000000000000000, -0.000000000000000000 ) ) ;
#12686=CARTESIAN_POINT ( 'NONE',  ( -55.99999999999989342, 493.2350855268086320, -521.8755148539809170 ) ) ;
#12689=CARTESIAN_POINT ( 'NONE',  ( -46.99999999999988631, 559.9933750504617365, -542.0276205133087615 ) ) ;
#12705=AXIS2_PLACEMENT_3D ( 'NONE', #6540, #16688, #10265 ) ;
#12707=FACE_BOUND ( 'NONE', #7249, .T. ) ;
#12709=ORIENTED_EDGE ( 'NONE', *, *, #8324, .F. ) ;
#12711=CARTESIAN_POINT ( 'NONE',  ( -55.99999999999989342, 523.2161522479888163, -489.1982331128240276 ) ) ;
#12715=AXIS2_PLACEMENT_3D ( 'NONE', #7052, #14804, #14883 ) ;
#12725=AXIS2_PLACEMENT_3D ( 'NONE', #7769, #15675, #4013 ) ;
#12730=DIRECTION ( 'NONE',  ( -1.000000000000000000, 0.000000000000000000, 0.000000000000000000 ) ) ;
#12734=CARTESIAN_POINT ( 'NONE',  ( -55.99999999999989342, 549.5810598491746077, -504.4200196135282113 ) ) ;
#12736=VERTEX_POINT ( 'NONE', #2909 ) ;
#12741=ORIENTED_EDGE ( 'NONE', *, *, #13635, .T. ) ;
#12751=CARTESIAN_POINT ( 'NONE',  ( 54.99999999999999289, 515.4878487013597805, -546.7230258972048205 ) ) ;
#12752=ORIENTED_EDGE ( 'NONE', *, *, #11387, .F. ) ;
#12758=ORIENTED_EDGE ( 'NONE', *, *, #6231, .T. ) ;
#12761=AXIS2_PLACEMENT_3D ( 'NONE', #5570, #7884, #13137 ) ;
#12762=ORIENTED_EDGE ( 'NONE', *, *, #2268, .T. ) ;
#12779=FACE_OUTER_BOUND ( 'NONE', #12580, .T. ) ;
#12784=CARTESIAN_POINT ( 'NONE',  ( -55.99999999999989342, 473.6663340069157471, -531.5012393965008641 ) ) ;
#12788=ADVANCED_FACE ( 'NONE', ( #4613 ), #4779, .T. ) ;
#12790=CARTESIAN_POINT ( 'NONE',  ( -45.00000000000000000, 473.6663340069158039, -561.9448123979092315 ) ) ;
#12792=CARTESIAN_POINT ( 'NONE',  ( -55.99999999999989342, 549.5810598491746077, -518.1154249974242703 ) ) ;
#12796=AXIS2_PLACEMENT_3D ( 'NONE', #11061, #3333, #11147 ) ;
#12799=FACE_OUTER_BOUND ( 'NONE', #16247, .T. ) ;
#12808=AXIS2_PLACEMENT_3D ( 'NONE', #2284, #14465, #3990 ) ;
#12815=ORIENTED_EDGE ( 'NONE', *, *, #3072, .F. ) ;
#12827=DIRECTION ( 'NONE',  ( -1.000000000000000000, 0.000000000000000000, -0.000000000000000000 ) ) ;
#12830=EDGE_CURVE ( 'NONE', #3860, #6348, #1369, .T. ) ;
#12836=ORIENTED_EDGE ( 'NONE', *, *, #13422, .F. ) ;
#12837=PLANE ( 'NONE',  #6861 ) ;
#12839=EDGE_LOOP ( 'NONE', ( #13640, #12233 ) ) ;
#12842=AXIS2_PLACEMENT_3D ( 'NONE', #486, #8460, #5877 ) ;
#12843=ORIENTED_EDGE ( 'NONE', *, *, #13269, .T. ) ;
#12848=ORIENTED_EDGE ( 'NONE', *, *, #3841, .T. ) ;
#12851=AXIS2_PLACEMENT_3D ( 'NONE', #8504, #12455, #9879 ) ;
#12854=DIRECTION ( 'NONE',  ( 0.000000000000000000, -0.8660254037844363761, -0.5000000000000039968 ) ) ;
#12857=ADVANCED_FACE ( 'NONE', ( #8408 ), #13463, .T. ) ;
#12861=DIRECTION ( 'NONE',  ( 1.000000000000000000, -0.000000000000000000, -0.000000000000000000 ) ) ;
#12863=VERTEX_POINT ( 'NONE', #7765 ) ;
#12865=AXIS2_PLACEMENT_3D ( 'NONE', #2178, #14035, #14129 ) ;
#12866=CARTESIAN_POINT ( 'NONE',  ( -55.99999999999988631, 172.2913238082672933, 146.1547335252150788 ) ) ;
#12876=ORIENTED_EDGE ( 'NONE', *, *, #2254, .T. ) ;
#12888=ORIENTED_EDGE ( 'NONE', *, *, #7393, .F. ) ;
#12894=FACE_OUTER_BOUND ( 'NONE', #383, .T. ) ;
#12895=ORIENTED_EDGE ( 'NONE', *, *, #6410, .T. ) ;
#12919=ORIENTED_EDGE ( 'NONE', *, *, #9608, .F. ) ;
#12925=ORIENTED_EDGE ( 'NONE', *, *, #11404, .F. ) ;
#12932=LINE ( 'NONE', #14059, #3752 ) ;
#12933=DIRECTION ( 'NONE',  ( 0.000000000000000000, 0.000000000000000000, 1.000000000000000000 ) ) ;
#12937=ORIENTED_EDGE ( 'NONE', *, *, #6022, .T. ) ;
#12940=AXIS2_PLACEMENT_3D ( 'NONE', #4203, #6768, #8228 ) ;
#12941=DIRECTION ( 'NONE',  ( 0.000000000000000000, 0.000000000000000000, -1.000000000000000000 ) ) ;
#12944=AXIS2_PLACEMENT_3D ( 'NONE', #8915, #9072, #12933 ) ;
#12945=AXIS2_PLACEMENT_3D ( 'NONE', #15796, #15626, #14341 ) ;
#12952=CARTESIAN_POINT ( 'NONE',  ( 45.00000000000000000, 473.6663340069157471, -517.8058340126048051 ) ) ;
#12955=VERTEX_POINT ( 'NONE', #4940 ) ;
#12959=CARTESIAN_POINT ( 'NONE',  ( 45.00000000000000000, 493.2350855268086320, -494.4847040861889127 ) ) ;
#12960=EDGE_LOOP ( 'NONE', ( #15265, #2138, #10586, #16065 ) ) ;
#12973=ADVANCED_FACE ( 'NONE', ( #10192 ), #11551, .F. ) ;
#12978=ORIENTED_EDGE ( 'NONE', *, *, #1855, .F. ) ;
#12980=EDGE_CURVE ( 'NONE', #9616, #13962, #8511, .T. ) ;
#12985=ORIENTED_EDGE ( 'NONE', *, *, #4784, .F. ) ;
#12986=VERTEX_POINT ( 'NONE', #15428 ) ;
#12991=VERTEX_POINT ( 'NONE', #16631 ) ;
#12994=CIRCLE ( 'NONE', #5309, 4.695405383896011919 ) ;
#12998=VECTOR ( 'NONE', #802, 1000.000000000000000 ) ;
#13004=CIRCLE ( 'NONE', #399, 13.69540538389601991 ) ;
#13007=CARTESIAN_POINT ( 'NONE',  ( -45.00000000000000000, 473.6663340069157471, -517.8058340126048051 ) ) ;
#13012=ORIENTED_EDGE ( 'NONE', *, *, #4663, .T. ) ;
#13018=EDGE_LOOP ( 'NONE', ( #3178, #14639, #43, #13860, #14452 ) ) ;
#13023=EDGE_LOOP ( 'NONE', ( #1928, #10431, #2670, #1666 ) ) ;
#13026=DIRECTION ( 'NONE',  ( -1.000000000000000000, 0.000000000000000000, 0.000000000000000000 ) ) ;
#13027=DIRECTION ( 'NONE',  ( 0.000000000000000000, 0.000000000000000000, -1.000000000000000000 ) ) ;
#13029=DIRECTION ( 'NONE',  ( 1.000000000000000000, 0.000000000000000000, 0.000000000000000000 ) ) ;
#13038=EDGE_CURVE ( 'NONE', #8101, #3466, #2718, .T. ) ;
#13063=CARTESIAN_POINT ( 'NONE',  ( 46.99999999999988631, 549.5810598491749488, -575.3306267969850296 ) ) ;
#13064=EDGE_LOOP ( 'NONE', ( #761, #13345, #10816, #7 ) ) ;
#13065=DIRECTION ( 'NONE',  ( -1.000000000000000000, 0.000000000000000000, 0.000000000000000000 ) ) ;
#13068=DIRECTION ( 'NONE',  ( -1.000000000000000000, -0.000000000000000000, -0.000000000000000000 ) ) ;
#13085=VERTEX_POINT ( 'NONE', #14661 ) ;
#13086=DIRECTION ( 'NONE',  ( 1.000000000000000000, -0.000000000000000000, -0.000000000000000000 ) ) ;
#13093=VERTEX_POINT ( 'NONE', #2710 ) ;
#13096=ORIENTED_EDGE ( 'NONE', *, *, #15672, .T. ) ;
#13098=ORIENTED_EDGE ( 'NONE', *, *, #9295, .F. ) ;
#13105=ORIENTED_EDGE ( 'NONE', *, *, #11588, .F. ) ;
#13107=DIRECTION ( 'NONE',  ( 0.000000000000000000, 0.000000000000000000, -1.000000000000000000 ) ) ;
#13113=FACE_BOUND ( 'NONE', #10580, .T. ) ;
#13115=CIRCLE ( 'NONE', #6562, 13.69540538389601991 ) ;
#13125=ORIENTED_EDGE ( 'NONE', *, *, #16926, .F. ) ;
#13128=LINE ( 'NONE', #12866, #1830 ) ;
#13134=CARTESIAN_POINT ( 'NONE',  ( 49.99999999999999289, 515.4878487013597805, -631.7230258972047068 ) ) ;
#13136=EDGE_LOOP ( 'NONE', ( #16502, #5207, #2576, #14108 ) ) ;
#13137=DIRECTION ( 'NONE',  ( 0.000000000000000000, 0.000000000000000000, 1.000000000000000000 ) ) ;
#13145=DIRECTION ( 'NONE',  ( 0.000000000000000000, 0.000000000000000000, 1.000000000000000000 ) ) ;
#13158=EDGE_LOOP ( 'NONE', ( #5413, #3753, #16673, #8875 ) ) ;
#13164=FACE_OUTER_BOUND ( 'NONE', #2940, .T. ) ;
#13173=EDGE_CURVE ( 'NONE', #16404, #2588, #7916, .T. ) ;
#13174=EDGE_CURVE ( 'NONE', #750, #7474, #6266, .T. ) ;
#13175=DIRECTION ( 'NONE',  ( 1.000000000000000000, 0.000000000000000000, 0.000000000000000000 ) ) ;
#13184=ORIENTED_EDGE ( 'NONE', *, *, #10040, .T. ) ;
#13190=ORIENTED_EDGE ( 'NONE', *, *, #5476, .F. ) ;
#13200=DIRECTION ( 'NONE',  ( 0.000000000000000000, 0.000000000000000000, -1.000000000000000000 ) ) ;
#13205=DIRECTION ( 'NONE',  ( 1.000000000000000000, 0.000000000000000000, 0.000000000000000000 ) ) ;
#13209=FACE_OUTER_BOUND ( 'NONE', #13018, .T. ) ;
#13215=EDGE_CURVE ( 'NONE', #12955, #11618, #10163, .T. ) ;
#13218=CIRCLE ( 'NONE', #6607, 9.000000000000007105 ) ;
#13225=AXIS2_PLACEMENT_3D ( 'NONE', #3489, #14922, #3165 ) ;
#13226=DIRECTION ( 'NONE',  ( 0.000000000000000000, 0.000000000000000000, -1.000000000000000000 ) ) ;
#13238=FACE_OUTER_BOUND ( 'NONE', #7734, .T. ) ;
#13242=ORIENTED_EDGE ( 'NONE', *, *, #6410, .F. ) ;
#13259=CARTESIAN_POINT ( 'NONE',  ( 46.99999999999988631, 559.9933750504617365, -546.7230258972048205 ) ) ;
#13265=ORIENTED_EDGE ( 'NONE', *, *, #16722, .T. ) ;
#13268=ORIENTED_EDGE ( 'NONE', *, *, #2367, .F. ) ;
#13269=EDGE_CURVE ( 'NONE', #14463, #7690, #16734, .T. ) ;
#13270=DIRECTION ( 'NONE',  ( 1.000000000000000000, -0.000000000000000000, -0.000000000000000000 ) ) ;
#13275=AXIS2_PLACEMENT_3D ( 'NONE', #3796, #2492, #10486 ) ;
#13284=DIRECTION ( 'NONE',  ( 0.000000000000000000, 0.000000000000000000, 1.000000000000000000 ) ) ;
#13287=CIRCLE ( 'NONE', #11628, 9.000000000000007105 ) ;
#13295=AXIS2_PLACEMENT_3D ( 'NONE', #5161, #10413, #15646 ) ;
#13301=EDGE_CURVE ( 'NONE', #9122, #6264, #15063, .T. ) ;
#13304=DIRECTION ( 'NONE',  ( 0.000000000000000000, 0.000000000000000000, -1.000000000000000000 ) ) ;
#13309=CARTESIAN_POINT ( 'NONE',  ( 45.00000000000000000, 549.5810598491749488, -575.3306267969850296 ) ) ;
#13315=CARTESIAN_POINT ( 'NONE',  ( 54.99999999999999289, 515.4878487013597805, -631.7230258972047068 ) ) ;
#13322=ADVANCED_FACE ( 'NONE', ( #8389 ), #567, .T. ) ;
#13326=FACE_OUTER_BOUND ( 'NONE', #8264, .T. ) ;
#13331=VERTEX_POINT ( 'NONE', #2258 ) ;
#13332=FACE_OUTER_BOUND ( 'NONE', #10020, .T. ) ;
#13339=EDGE_LOOP ( 'NONE', ( #13518, #6835, #10928, #9020 ) ) ;
#13341=ORIENTED_EDGE ( 'NONE', *, *, #2367, .T. ) ;
#13344=VECTOR ( 'NONE', #11418, 1000.000000000000000 ) ;
#13345=ORIENTED_EDGE ( 'NONE', *, *, #13389, .T. ) ;
#13355=DIRECTION ( 'NONE',  ( 0.000000000000000000, 0.000000000000000000, -1.000000000000000000 ) ) ;
#13368=AXIS2_PLACEMENT_3D ( 'NONE', #9769, #13959, #5965 ) ;
#13371=DIRECTION ( 'NONE',  ( 0.000000000000000000, 0.000000000000000000, -1.000000000000000000 ) ) ;
#13382=TOROIDAL_SURFACE ( 'NONE', #7589, 4.695405383895982609, 9.000000000000000000 ) ;
#13389=EDGE_CURVE ( 'NONE', #13923, #8117, #3735, .T. ) ;
#13391=CARTESIAN_POINT ( 'NONE',  ( -46.99999999999988631, 473.6663340069158039, -548.2494070140132862 ) ) ;
#13392=DIRECTION ( 'NONE',  ( -1.000000000000000000, 0.000000000000000000, 0.000000000000000000 ) ) ;
#13402=CARTESIAN_POINT ( 'NONE',  ( -46.99999999999988631, 549.5810598491746077, -522.8108303813202156 ) ) ;
#13416=EDGE_LOOP ( 'NONE', ( #1331, #10922 ) ) ;
#13422=EDGE_CURVE ( 'NONE', #13093, #12214, #537, .T. ) ;
#13427=ORIENTED_EDGE ( 'NONE', *, *, #10786, .T. ) ;
#13443=DIRECTION ( 'NONE',  ( -1.000000000000000000, 0.000000000000000000, 0.000000000000000000 ) ) ;
#13449=CIRCLE ( 'NONE', #2189, 4.695405383896011919 ) ;
#13450=VERTEX_POINT ( 'NONE', #12629 ) ;
#13460=DIRECTION ( 'NONE',  ( 0.000000000000000000, 0.000000000000000000, -1.000000000000000000 ) ) ;
#13461=CARTESIAN_POINT ( 'NONE',  ( 49.99999999999999289, 515.4878487013597805, -606.7230258972047068 ) ) ;
#13463=TOROIDAL_SURFACE ( 'NONE', #9607, 4.695405383895982609, 9.000000000000000000 ) ;
#13470=DIRECTION ( 'NONE',  ( 0.000000000000000000, -0.3420201433256630508, -0.9396926207859104263 ) ) ;
#13472=PLANE ( 'NONE',  #1740 ) ;
#13474=VERTEX_POINT ( 'NONE', #14968 ) ;
#13478=CARTESIAN_POINT ( 'NONE',  ( 46.99999999999988631, 493.2350855268092573, -585.2659423243250103 ) ) ;
#13480=CARTESIAN_POINT ( 'NONE',  ( -49.99999999999999289, 515.4878487013597805, -546.7230258972048205 ) ) ;
#13486=DIRECTION ( 'NONE',  ( 0.000000000000000000, 0.8660254037844432595, -0.4999999999999919509 ) ) ;
#13494=ORIENTED_EDGE ( 'NONE', *, *, #280, .F. ) ;
#13497=DIRECTION ( 'NONE',  ( 0.000000000000000000, 1.000000000000000000, -1.224646799147353207E-16 ) ) ;
#13498=VERTEX_POINT ( 'NONE', #1826 ) ;
#13500=AXIS2_PLACEMENT_3D ( 'NONE', #12784, #10887, #13470 ) ;
#13505=ORIENTED_EDGE ( 'NONE', *, *, #12664, .F. ) ;
#13506=AXIS2_PLACEMENT_3D ( 'NONE', #15645, #1392, #5160 ) ;
#13511=VECTOR ( 'NONE', #3827, 1000.000000000000000 ) ;
#13515=VECTOR ( 'NONE', #4002, 1000.000000000000000 ) ;
#13516=LINE ( 'NONE', #8094, #4166 ) ;
#13518=ORIENTED_EDGE ( 'NONE', *, *, #14354, .F. ) ;
#13532=ORIENTED_EDGE ( 'NONE', *, *, #15050, .F. ) ;
#13534=ORIENTED_EDGE ( 'NONE', *, *, #8121, .F. ) ;
#13535=CARTESIAN_POINT ( 'NONE',  ( -45.00000000000000000, 523.2161522479893847, -576.8570079137933817 ) ) ;
#13537=DIRECTION ( 'NONE',  ( -1.000000000000000000, 0.000000000000000000, -0.000000000000000000 ) ) ;
#13538=FACE_OUTER_BOUND ( 'NONE', #7270, .T. ) ;
#13550=DIRECTION ( 'NONE',  ( 0.000000000000000000, 0.000000000000000000, 1.000000000000000000 ) ) ;
#13561=ORIENTED_EDGE ( 'NONE', *, *, #3733, .F. ) ;
#13564=DIRECTION ( 'NONE',  ( 1.000000000000000000, -0.000000000000000000, -0.000000000000000000 ) ) ;
#13566=DIRECTION ( 'NONE',  ( 0.000000000000000000, 0.000000000000000000, -1.000000000000000000 ) ) ;
#13572=ORIENTED_EDGE ( 'NONE', *, *, #1292, .T. ) ;
#13583=CYLINDRICAL_SURFACE ( 'NONE', #9222, 13.69540538389601991 ) ;
#13599=VERTEX_POINT ( 'NONE', #1804 ) ;
#13601=EDGE_LOOP ( 'NONE', ( #12279, #8700, #3250, #2680 ) ) ;
#13614=CARTESIAN_POINT ( 'NONE',  ( 45.00000000000000000, 523.2161522479888163, -489.1982331128240276 ) ) ;
#13618=ORIENTED_EDGE ( 'NONE', *, *, #15050, .T. ) ;
#13621=ORIENTED_EDGE ( 'NONE', *, *, #8464, .F. ) ;
#13635=EDGE_CURVE ( 'NONE', #14813, #2243, #1628, .T. ) ;
#13640=ORIENTED_EDGE ( 'NONE', *, *, #14983, .T. ) ;
#13653=PLANE ( 'NONE',  #4799 ) ;
#13655=EDGE_LOOP ( 'NONE', ( #9697, #5574 ) ) ;
#13656=DIRECTION ( 'NONE',  ( 1.000000000000000000, -0.000000000000000000, 0.000000000000000000 ) ) ;
#13658=DIRECTION ( 'NONE',  ( 0.000000000000000000, -1.000000000000000000, 0.000000000000000000 ) ) ;
#13664=VERTEX_POINT ( 'NONE', #12198 ) ;
#13672=ORIENTED_EDGE ( 'NONE', *, *, #3427, .F. ) ;
#13674=TOROIDAL_SURFACE ( 'NONE', #12572, 4.695405383895982609, 9.000000000000000000 ) ;
#13677=EDGE_LOOP ( 'NONE', ( #2180, #13427, #16011, #12566 ) ) ;
#13683=ORIENTED_EDGE ( 'NONE', *, *, #8882, .T. ) ;
#13686=DIRECTION ( 'NONE',  ( -1.000000000000000000, -0.000000000000000000, -0.000000000000000000 ) ) ;
#13692=ADVANCED_FACE ( 'NONE', ( #5397 ), #12022, .F. ) ;
#13698=CARTESIAN_POINT ( 'NONE',  ( 45.00000000000000000, 515.4878487013597805, -546.7230258972048205 ) ) ;
#13708=DIRECTION ( 'NONE',  ( -0.000000000000000000, 0.7625786632508375629, 0.6468954956981580739 ) ) ;
#13713=DIRECTION ( 'NONE',  ( 0.000000000000000000, 0.000000000000000000, -1.000000000000000000 ) ) ;
#13717=CARTESIAN_POINT ( 'NONE',  ( -55.99999999999988631, 645.2345343053611941, -411.3640676610526157 ) ) ;
#13727=CARTESIAN_POINT ( 'NONE',  ( -45.00000000000000000, 523.2161522479888163, -502.8936384967199729 ) ) ;
#13730=DIRECTION ( 'NONE',  ( 1.000000000000000000, 0.000000000000000000, -0.000000000000000000 ) ) ;
#13733=FACE_OUTER_BOUND ( 'NONE', #16198, .T. ) ;
#13737=DIRECTION ( 'NONE',  ( 0.000000000000000000, 0.000000000000000000, -1.000000000000000000 ) ) ;
#13743=DIRECTION ( 'NONE',  ( 0.000000000000000000, 0.000000000000000000, 1.000000000000000000 ) ) ;
#13747=AXIS2_PLACEMENT_3D ( 'NONE', #9339, #958, #6176 ) ;
#13754=AXIS2_PLACEMENT_3D ( 'NONE', #2785, #11805, #6294 ) ;
#13766=AXIS2_PLACEMENT_3D ( 'NONE', #1985, #7380, #2231 ) ;
#13767=ADVANCED_FACE ( 'NONE', ( #15194 ), #8583, .T. ) ;
#13780=EDGE_CURVE ( 'NONE', #1044, #8336, #6546, .T. ) ;
#13785=ORIENTED_EDGE ( 'NONE', *, *, #3362, .F. ) ;
#13798=CARTESIAN_POINT ( 'NONE',  ( -55.99999999999989342, 473.6663340069158039, -575.6402177818052905 ) ) ;
#13801=DIRECTION ( 'NONE',  ( 1.000000000000000000, 0.000000000000000000, 0.000000000000000000 ) ) ;
#13803=DIRECTION ( 'NONE',  ( 0.000000000000000000, 0.000000000000000000, 1.000000000000000000 ) ) ;
#13815=ADVANCED_FACE ( 'NONE', ( #4792 ), #7104, .T. ) ;
#13816=ADVANCED_FACE ( 'NONE', ( #12527 ), #12067, .T. ) ;
#13819=EDGE_CURVE ( 'NONE', #6925, #6110, #14246, .T. ) ;
#13822=ORIENTED_EDGE ( 'NONE', *, *, #12551, .T. ) ;
#13827=CARTESIAN_POINT ( 'NONE',  ( 46.99999999999988631, 523.2161522479888163, -502.8936384967199729 ) ) ;
#13835=VECTOR ( 'NONE', #3600, 1000.000000000000000 ) ;
#13853=VERTEX_POINT ( 'NONE', #11823 ) ;
#13860=ORIENTED_EDGE ( 'NONE', *, *, #2242, .T. ) ;
#13862=TOROIDAL_SURFACE ( 'NONE', #2617, 4.695405383895982609, 9.000000000000000000 ) ;
#13863=DIRECTION ( 'NONE',  ( 0.000000000000000000, 0.000000000000000000, -1.000000000000000000 ) ) ;
#13866=CARTESIAN_POINT ( 'NONE',  ( -55.99999999999989342, 523.2161522479893847, -595.2478186815853860 ) ) ;
#13870=FACE_BOUND ( 'NONE', #14279, .T. ) ;
#13874=AXIS2_PLACEMENT_3D ( 'NONE', #8861, #3544, #7220 ) ;
#13881=DIRECTION ( 'NONE',  ( 1.000000000000000000, -0.000000000000000000, 0.000000000000000000 ) ) ;
#13884=DIRECTION ( 'NONE',  ( 0.000000000000000000, 0.000000000000000000, 1.000000000000000000 ) ) ;
#13897=ORIENTED_EDGE ( 'NONE', *, *, #8624, .T. ) ;
#13898=VECTOR ( 'NONE', #6760, 1000.000000000000000 ) ;
#13900=AXIS2_PLACEMENT_3D ( 'NONE', #14627, #11107, #4413 ) ;
#13901=CARTESIAN_POINT ( 'NONE',  ( -45.00000000000000000, 549.5810598491746077, -518.1154249974242703 ) ) ;
#13903=VERTEX_POINT ( 'NONE', #2380 ) ;
#13904=EDGE_CURVE ( 'NONE', #16578, #7039, #8550, .T. ) ;
#13907=ORIENTED_EDGE ( 'NONE', *, *, #7338, .T. ) ;
#13909=EDGE_CURVE ( 'NONE', #750, #14463, #15127, .T. ) ;
#13916=EDGE_CURVE ( 'NONE', #13331, #1995, #11288, .T. ) ;
#13923=VERTEX_POINT ( 'NONE', #6398 ) ;
#13933=ADVANCED_FACE ( 'NONE', ( #6484 ), #11483, .T. ) ;
#13934=ADVANCED_FACE ( 'NONE', ( #1022 ), #10453, .T. ) ;
#13937=ADVANCED_FACE ( 'NONE', ( #10706 ), #4281, .F. ) ;
#13943=VERTEX_POINT ( 'NONE', #1690 ) ;
#13959=DIRECTION ( 'NONE',  ( 0.000000000000000000, -1.000000000000000000, 0.000000000000000000 ) ) ;
#13961=CARTESIAN_POINT ( 'NONE',  ( 55.99999999999989342, 559.9933750504617365, -546.7230258972048205 ) ) ;
#13962=VERTEX_POINT ( 'NONE', #8301 ) ;
#13966=DIRECTION ( 'NONE',  ( -1.000000000000000000, -0.000000000000000000, -0.000000000000000000 ) ) ;
#13972=CARTESIAN_POINT ( 'NONE',  ( -55.99999999999989342, 549.5810598491746077, -531.8108303813202156 ) ) ;
#13977=DIRECTION ( 'NONE',  ( 0.000000000000000000, 0.9848077530122061329, 0.1736481776669406840 ) ) ;
#13981=ORIENTED_EDGE ( 'NONE', *, *, #13819, .F. ) ;
#14002=AXIS2_PLACEMENT_3D ( 'NONE', #1043, #13068, #6593 ) ;
#14004=AXIS2_PLACEMENT_3D ( 'NONE', #1857, #3230, #14825 ) ;
#14011=CIRCLE ( 'NONE', #5504, 13.69540538389601991 ) ;
#14017=EDGE_CURVE ( 'NONE', #15832, #1196, #9666, .T. ) ;
#14022=EDGE_CURVE ( 'NONE', #11869, #12394, #11295, .T. ) ;
#14026=EDGE_CURVE ( 'NONE', #12863, #2782, #6892, .T. ) ;
#14027=ORIENTED_EDGE ( 'NONE', *, *, #4134, .F. ) ;
#14028=ORIENTED_EDGE ( 'NONE', *, *, #9516, .T. ) ;
#14029=CARTESIAN_POINT ( 'NONE',  ( -55.99999999999988631, 658.4713480608917280, -425.4301204538002139 ) ) ;
#14035=DIRECTION ( 'NONE',  ( 1.000000000000000000, 0.000000000000000000, -0.000000000000000000 ) ) ;
#14042=DIRECTION ( 'NONE',  ( 0.000000000000000000, 0.000000000000000000, -1.000000000000000000 ) ) ;
#14046=ADVANCED_FACE ( 'NONE', ( #6050 ), #9777, .T. ) ;
#14054=CIRCLE ( 'NONE', #885, 9.000000000000007105 ) ;
#14059=CARTESIAN_POINT ( 'NONE',  ( -55.99999999999988631, 173.0499717945046996, 146.7982946275220968 ) ) ;
#14061=CIRCLE ( 'NONE', #1171, 4.695405383896011919 ) ;
#14066=TOROIDAL_SURFACE ( 'NONE', #3367, 4.695405383895982609, 9.000000000000000000 ) ;
#14067=DIRECTION ( 'NONE',  ( 1.000000000000000000, -0.000000000000000000, -0.000000000000000000 ) ) ;
#14068=PRESENTATION_STYLE_ASSIGNMENT (( #6070 ) ) ;
#14074=EDGE_LOOP ( 'NONE', ( #14434, #10678, #15720, #6852 ) ) ;
#14077=CIRCLE ( 'NONE', #14633, 9.000000000000007105 ) ;
#14098=CARTESIAN_POINT ( 'NONE',  ( 46.99999999999988631, 549.5810598491749488, -570.6352214130889706 ) ) ;
#14108=ORIENTED_EDGE ( 'NONE', *, *, #5992, .T. ) ;
#14129=DIRECTION ( 'NONE',  ( 0.000000000000000000, 0.6427876096865299260, 0.7660444431189857850 ) ) ;
#14138=EDGE_LOOP ( 'NONE', ( #2169, #966 ) ) ;
#14167=DIRECTION ( 'NONE',  ( 1.000000000000000000, -0.000000000000000000, -0.000000000000000000 ) ) ;
#14172=AXIS2_PLACEMENT_3D ( 'NONE', #16212, #252, #10900 ) ;
#14188=CARTESIAN_POINT ( 'NONE',  ( -45.00000000000000000, 549.5810598491749488, -575.3306267969850296 ) ) ;
#14191=ORIENTED_EDGE ( 'NONE', *, *, #6489, .T. ) ;
#14202=CARTESIAN_POINT ( 'NONE',  ( -55.99999999999989342, 523.2161522479888163, -502.8936384967199729 ) ) ;
#14203=DIRECTION ( 'NONE',  ( 0.000000000000000000, 0.000000000000000000, -1.000000000000000000 ) ) ;
#14204=ORIENTED_EDGE ( 'NONE', *, *, #2335, .F. ) ;
#14209=ORIENTED_EDGE ( 'NONE', *, *, #2254, .F. ) ;
#14215=VERTEX_POINT ( 'NONE', #15842 ) ;
#14233=EDGE_CURVE ( 'NONE', #16590, #8336, #1332, .T. ) ;
#14241=CARTESIAN_POINT ( 'NONE',  ( -46.99999999999988631, 523.2161522479888163, -502.8936384967199729 ) ) ;
#14246=CIRCLE ( 'NONE', #6826, 13.69540538389598439 ) ;
#14250=DIRECTION ( 'NONE',  ( 0.000000000000000000, 0.000000000000000000, 1.000000000000000000 ) ) ;
#14252=VERTEX_POINT ( 'NONE', #13535 ) ;
#14253=LINE ( 'NONE', #12711, #10158 ) ;
#14255=EDGE_LOOP ( 'NONE', ( #13907, #7151 ) ) ;
#14256=CARTESIAN_POINT ( 'NONE',  ( -46.99999999999988631, 473.6663340069157471, -531.5012393965008641 ) ) ;
#14257=AXIS2_PLACEMENT_3D ( 'NONE', #179, #10642, #13226 ) ;
#14259=EDGE_CURVE ( 'NONE', #12986, #12394, #7185, .T. ) ;
#14263=DIRECTION ( 'NONE',  ( 0.000000000000000000, 1.000000000000000000, -1.224646799147353207E-16 ) ) ;
#14264=ORIENTED_EDGE ( 'NONE', *, *, #9738, .F. ) ;
#14268=AXIS2_PLACEMENT_3D ( 'NONE', #4276, #320, #15852 ) ;
#14272=ORIENTED_EDGE ( 'NONE', *, *, #2311, .T. ) ;
#14279=EDGE_LOOP ( 'NONE', ( #1489, #6440 ) ) ;
#14281=CARTESIAN_POINT ( 'NONE',  ( 45.00000000000000000, 515.4878487013597805, -546.7230258972048205 ) ) ;
#14286=VERTEX_POINT ( 'NONE', #16512 ) ;
#14307=FACE_BOUND ( 'NONE', #5364, .T. ) ;
#14327=CARTESIAN_POINT ( 'NONE',  ( -46.99999999999988631, 473.6663340069157471, -545.1966447803968094 ) ) ;
#14335=CARTESIAN_POINT ( 'NONE',  ( 55.99999999999989342, 523.2161522479888163, -502.8936384967199729 ) ) ;
#14341=DIRECTION ( 'NONE',  ( 0.000000000000000000, 0.000000000000000000, -1.000000000000000000 ) ) ;
#14352=DIRECTION ( 'NONE',  ( -1.000000000000000000, 0.000000000000000000, 0.000000000000000000 ) ) ;
#14354=EDGE_CURVE ( 'NONE', #15297, #11097, #16354, .T. ) ;
#14360=CIRCLE ( 'NONE', #6116, 9.000000000000007105 ) ;
#14361=CIRCLE ( 'NONE', #3663, 4.695405383896011919 ) ;
#14374=CARTESIAN_POINT ( 'NONE',  ( -54.99999999999999289, 515.4878487013597805, -546.7230258972048205 ) ) ;
#14379=DIRECTION ( 'NONE',  ( -1.000000000000000000, -0.000000000000000000, -0.000000000000000000 ) ) ;
#14382=ORIENTED_EDGE ( 'NONE', *, *, #241, .F. ) ;
#14388=VERTEX_POINT ( 'NONE', #10473 ) ;
#14389=ORIENTED_EDGE ( 'NONE', *, *, #4995, .F. ) ;
#14391=AXIS2_PLACEMENT_3D ( 'NONE', #7795, #11759, #10389 ) ;
#14394=DIRECTION ( 'NONE',  ( -1.000000000000000000, -0.000000000000000000, -0.000000000000000000 ) ) ;
#14395=EDGE_LOOP ( 'NONE', ( #15694, #3133, #3445, #2773 ) ) ;
#14401=FACE_OUTER_BOUND ( 'NONE', #13655, .T. ) ;
#14404=FACE_OUTER_BOUND ( 'NONE', #12173, .T. ) ;
#14408=EDGE_CURVE ( 'NONE', #11618, #12955, #16249, .T. ) ;
#14411=CARTESIAN_POINT ( 'NONE',  ( -49.99999999999999289, 515.4878487013597805, -631.7230258972047068 ) ) ;
#14422=CARTESIAN_POINT ( 'NONE',  ( 55.99999999999989342, 493.2350855268092573, -585.2659423243250103 ) ) ;
#14423=CARTESIAN_POINT ( 'NONE',  ( -54.99999999999999289, 645.2345343053611941, -411.3640676610526157 ) ) ;
#14428=AXIS2_PLACEMENT_3D ( 'NONE', #3487, #2188, #1154 ) ;
#14429=ADVANCED_FACE ( 'NONE', ( #180 ), #15139, .T. ) ;
#14433=EDGE_CURVE ( 'NONE', #15367, #15832, #3471, .T. ) ;
#14434=ORIENTED_EDGE ( 'NONE', *, *, #13909, .F. ) ;
#14436=LINE ( 'NONE', #1210, #14875 ) ;
#14446=DIRECTION ( 'NONE',  ( 0.000000000000000000, 0.000000000000000000, -1.000000000000000000 ) ) ;
#14452=ORIENTED_EDGE ( 'NONE', *, *, #7002, .F. ) ;
#14463=VERTEX_POINT ( 'NONE', #11845 ) ;
#14465=DIRECTION ( 'NONE',  ( -1.000000000000000000, -0.000000000000000000, -0.000000000000000000 ) ) ;
#14466=AXIS2_PLACEMENT_3D ( 'NONE', #9571, #8104, #2864 ) ;
#14467=PLANE ( 'NONE',  #7753 ) ;
#14473=ORIENTED_EDGE ( 'NONE', *, *, #10841, .F. ) ;
#14482=CARTESIAN_POINT ( 'NONE',  ( -46.99999999999988631, 493.2350855268086320, -494.4847040861889127 ) ) ;
#14492=ADVANCED_FACE ( 'NONE', ( #13326 ), #14066, .T. ) ;
#14495=DIRECTION ( 'NONE',  ( 0.000000000000000000, 0.000000000000000000, -1.000000000000000000 ) ) ;
#14498=DIRECTION ( 'NONE',  ( -0.000000000000000000, -1.000000000000000000, 0.000000000000000000 ) ) ;
#14500=ORIENTED_EDGE ( 'NONE', *, *, #3760, .F. ) ;
#14503=DIRECTION ( 'NONE',  ( 0.000000000000000000, -0.6427876096865404731, 0.7660444431189771253 ) ) ;
#14508=DIRECTION ( 'NONE',  ( 0.000000000000000000, 0.000000000000000000, 1.000000000000000000 ) ) ;
#14509=CARTESIAN_POINT ( 'NONE',  ( -46.99999999999988631, 493.2350855268086320, -512.8755148539809170 ) ) ;
#14511=LINE ( 'NONE', #15792, #5892 ) ;
#14514=EDGE_LOOP ( 'NONE', ( #14500, #12937, #7125, #13494 ) ) ;
#14517=EDGE_CURVE ( 'NONE', #11329, #1995, #11315, .T. ) ;
#14518=DIRECTION ( 'NONE',  ( -1.000000000000000000, 0.000000000000000000, 0.000000000000000000 ) ) ;
#14522=DIRECTION ( 'NONE',  ( 0.000000000000000000, -1.000000000000000000, 0.000000000000000000 ) ) ;
#14523=VERTEX_POINT ( 'NONE', #9451 ) ;
#14525=ORIENTED_EDGE ( 'NONE', *, *, #10040, .F. ) ;
#14529=VERTEX_POINT ( 'NONE', #2829 ) ;
#14550=EDGE_CURVE ( 'NONE', #2782, #14286, #10992, .T. ) ;
#14553=CARTESIAN_POINT ( 'NONE',  ( -46.99999999999988631, 523.2161522479893847, -576.8570079137933817 ) ) ;
#14561=CYLINDRICAL_SURFACE ( 'NONE', #13754, 13.69540538389601991 ) ;
#14562=DIRECTION ( 'NONE',  ( 0.000000000000000000, 0.000000000000000000, -1.000000000000000000 ) ) ;
#14567=CARTESIAN_POINT ( 'NONE',  ( -46.99999999999988631, 523.2161522479888163, -507.5890438806159750 ) ) ;
#14569=DIRECTION ( 'NONE',  ( -1.000000000000000000, -0.000000000000000000, 0.000000000000000000 ) ) ;
#14582=DIRECTION ( 'NONE',  ( 1.000000000000000000, 0.000000000000000000, 0.000000000000000000 ) ) ;
#14584=CARTESIAN_POINT ( 'NONE',  ( -45.00000000000000000, 549.5810598491746077, -518.1154249974242703 ) ) ;
#14587=MANIFOLD_SOLID_BREP ( 'Boss-Extrude4', #7435 ) ;
#14612=CIRCLE ( 'NONE', #7737, 13.69540538389601991 ) ;
#14617=CIRCLE ( 'NONE', #354, 59.99999999999994316 ) ;
#14618=STYLED_ITEM ( 'NONE', ( #14068 ), #14587 ) ;
#14619=EDGE_LOOP ( 'NONE', ( #7530, #12762, #13265, #9850 ) ) ;
#14627=CARTESIAN_POINT ( 'NONE',  ( 45.00000000000000000, 549.5810598491746077, -518.1154249974242703 ) ) ;
#14633=AXIS2_PLACEMENT_3D ( 'NONE', #8216, #10801, #4284 ) ;
#14634=ORIENTED_EDGE ( 'NONE', *, *, #2728, .T. ) ;
#14638=DIRECTION ( 'NONE',  ( -1.000000000000000000, 0.000000000000000000, 0.000000000000000000 ) ) ;
#14639=ORIENTED_EDGE ( 'NONE', *, *, #10531, .F. ) ;
#14641=CIRCLE ( 'NONE', #653, 13.69540538389596485 ) ;
#14651=DIRECTION ( 'NONE',  ( 0.000000000000000000, 0.000000000000000000, 1.000000000000000000 ) ) ;
#14652=ADVANCED_FACE ( 'NONE', ( #10120 ), #6364, .T. ) ;
#14660=AXIS2_PLACEMENT_3D ( 'NONE', #5995, #15030, #8591 ) ;
#14661=CARTESIAN_POINT ( 'NONE',  ( -46.99999999999988631, 493.2350855268086320, -521.8755148539809170 ) ) ;
#14662=CARTESIAN_POINT ( 'NONE',  ( -55.99999999999989342, 473.6663340069158039, -548.2494070140132862 ) ) ;
#14670=ORIENTED_EDGE ( 'NONE', *, *, #5798, .T. ) ;
#14671=LINE ( 'NONE', #2804, #7001 ) ;
#14673=CARTESIAN_POINT ( 'NONE',  ( -54.99999999999999289, 515.4878487013597805, -631.7230258972047068 ) ) ;
#14679=EDGE_CURVE ( 'NONE', #12411, #13599, #2261, .T. ) ;
#14688=DIRECTION ( 'NONE',  ( 1.000000000000000000, 0.000000000000000000, -0.000000000000000000 ) ) ;
#14691=DIRECTION ( 'NONE',  ( 1.000000000000000000, -0.000000000000000000, 0.000000000000000000 ) ) ;
#14692=DIRECTION ( 'NONE',  ( 0.000000000000000000, 0.000000000000000000, 1.000000000000000000 ) ) ;
#14696=CYLINDRICAL_SURFACE ( 'NONE', #10474, 13.69540538389596485 ) ;
#14700=PLANE ( 'NONE',  #15038 ) ;
#14701=DIRECTION ( 'NONE',  ( 1.000000000000000000, 0.000000000000000000, 0.000000000000000000 ) ) ;
#14713=AXIS2_PLACEMENT_3D ( 'NONE', #10977, #5389, #6837 ) ;
#14714=ADVANCED_FACE ( 'NONE', ( #10296 ), #1722, .T. ) ;
#14742=CYLINDRICAL_SURFACE ( 'NONE', #12842, 187.4999999999998863 ) ;
#14751=DIRECTION ( 'NONE',  ( -1.000000000000000000, 0.000000000000000000, -0.000000000000000000 ) ) ;
#14754=VECTOR ( 'NONE', #11500, 1000.000000000000000 ) ;
#14769=DIRECTION ( 'NONE',  ( 0.000000000000000000, 0.000000000000000000, 1.000000000000000000 ) ) ;
#14770=FACE_OUTER_BOUND ( 'NONE', #1842, .T. ) ;
#14786=ORIENTED_EDGE ( 'NONE', *, *, #14884, .F. ) ;
#14792=CARTESIAN_POINT ( 'NONE',  ( -55.99999999999989342, 473.6663340069157471, -526.8058340126048051 ) ) ;
#14795=CARTESIAN_POINT ( 'NONE',  ( -46.99999999999988631, 473.6663340069157471, -517.8058340126048051 ) ) ;
#14804=DIRECTION ( 'NONE',  ( 1.000000000000000000, -0.000000000000000000, -0.000000000000000000 ) ) ;
#14806=CARTESIAN_POINT ( 'NONE',  ( 46.99999999999988631, 523.2161522479888163, -502.8936384967199729 ) ) ;
#14812=CARTESIAN_POINT ( 'NONE',  ( -46.99999999999988631, 523.2161522479888163, -502.8936384967199729 ) ) ;
#14813=VERTEX_POINT ( 'NONE', #14411 ) ;
#14825=DIRECTION ( 'NONE',  ( 0.000000000000000000, 0.000000000000000000, -1.000000000000000000 ) ) ;
#14842=DIRECTION ( 'NONE',  ( 0.000000000000000000, 0.000000000000000000, -1.000000000000000000 ) ) ;
#14844=DIRECTION ( 'NONE',  ( -0.000000000000000000, 1.000000000000000000, -1.224646799147353207E-16 ) ) ;
#14852=ORIENTED_EDGE ( 'NONE', *, *, #7641, .T. ) ;
#14860=ADVANCED_FACE ( 'NONE', ( #13209 ), #13472, .T. ) ;
#14862=DIRECTION ( 'NONE',  ( -1.000000000000000000, -0.000000000000000000, -0.000000000000000000 ) ) ;
#14864=CARTESIAN_POINT ( 'NONE',  ( 45.00000000000000000, 523.2161522479893847, -590.5524132976893270 ) ) ;
#14875=VECTOR ( 'NONE', #1041, 1000.000000000000000 ) ;
#14883=DIRECTION ( 'NONE',  ( 0.000000000000000000, 0.000000000000000000, -1.000000000000000000 ) ) ;
#14884=EDGE_CURVE ( 'NONE', #5839, #11618, #14077, .T. ) ;
#14885=DIRECTION ( 'NONE',  ( 0.000000000000000000, 0.000000000000000000, -1.000000000000000000 ) ) ;
#14891=DIRECTION ( 'NONE',  ( 0.000000000000000000, 0.000000000000000000, 1.000000000000000000 ) ) ;
#14904=CARTESIAN_POINT ( 'NONE',  ( 175.0000000000000568, 515.4878487013597805, -571.7230258972048205 ) ) ;
#14910=CARTESIAN_POINT ( 'NONE',  ( -55.99999999999989342, 473.6663340069157471, -531.5012393965008641 ) ) ;
#14911=DIRECTION ( 'NONE',  ( -1.000000000000000000, 0.000000000000000000, -0.000000000000000000 ) ) ;
#14915=VERTEX_POINT ( 'NONE', #15858 ) ;
#14922=DIRECTION ( 'NONE',  ( 1.000000000000000000, -0.000000000000000000, -0.000000000000000000 ) ) ;
#14923=CIRCLE ( 'NONE', #2024, 4.695405383896011919 ) ;
#14926=CIRCLE ( 'NONE', #116, 13.69540538389601991 ) ;
#14931=LINE ( 'NONE', #3170, #16641 ) ;
#14942=FACE_OUTER_BOUND ( 'NONE', #9239, .T. ) ;
#14948=AXIS2_PLACEMENT_3D ( 'NONE', #2652, #15373, #3609 ) ;
#14952=CARTESIAN_POINT ( 'NONE',  ( -55.99999999999989342, 523.2161522479888163, -502.8936384967199729 ) ) ;
#14954=DIRECTION ( 'NONE',  ( 0.000000000000000000, 0.000000000000000000, 1.000000000000000000 ) ) ;
#14961=CARTESIAN_POINT ( 'NONE',  ( 46.99999999999988631, 523.2161522479893847, -590.5524132976893270 ) ) ;
#14962=CIRCLE ( 'NONE', #3434, 187.4999999999998863 ) ;
#14968=CARTESIAN_POINT ( 'NONE',  ( -55.99999999999989342, 549.5810598491746077, -522.8108303813202156 ) ) ;
#14972=VERTEX_POINT ( 'NONE', #2902 ) ;
#14983=EDGE_CURVE ( 'NONE', #13664, #963, #9965, .T. ) ;
#14991=CARTESIAN_POINT ( 'NONE',  ( 54.99999999999999289, 515.4878487013597805, -461.7230258972048205 ) ) ;
#14996=CIRCLE ( 'NONE', #1268, 4.695405383896011919 ) ;
#14997=CARTESIAN_POINT ( 'NONE',  ( -45.00000000000000000, 515.4878487013597805, -546.7230258972048205 ) ) ;
#14998=VERTEX_POINT ( 'NONE', #15011 ) ;
#15003=FACE_OUTER_BOUND ( 'NONE', #7562, .T. ) ;
#15007=EDGE_CURVE ( 'NONE', #6541, #11430, #2546, .T. ) ;
#15009=CIRCLE ( 'NONE', #7576, 187.4999999999998863 ) ;
#15010=DIRECTION ( 'NONE',  ( 0.000000000000000000, 0.000000000000000000, -1.000000000000000000 ) ) ;
#15011=CARTESIAN_POINT ( 'NONE',  ( -46.99999999999988631, 473.6663340069158039, -575.6402177818052905 ) ) ;
#15014=EDGE_LOOP ( 'NONE', ( #13242, #15528 ) ) ;
#15017=DIRECTION ( 'NONE',  ( 0.000000000000000000, 0.000000000000000000, -1.000000000000000000 ) ) ;
#15021=DIRECTION ( 'NONE',  ( 1.000000000000000000, 0.000000000000000000, 0.000000000000000000 ) ) ;
#15022=CARTESIAN_POINT ( 'NONE',  ( 45.00000000000000000, 523.2161522479888163, -502.8936384967199729 ) ) ;
#15023=SURFACE_STYLE_FILL_AREA ( #5989 ) ;
#15030=DIRECTION ( 'NONE',  ( -1.000000000000000000, 0.000000000000000000, 0.000000000000000000 ) ) ;
#15032=DIRECTION ( 'NONE',  ( -1.000000000000000000, -0.000000000000000000, -0.000000000000000000 ) ) ;
#15036=VERTEX_POINT ( 'NONE', #12424 ) ;
#15038=AXIS2_PLACEMENT_3D ( 'NONE', #8167, #4314, #10483 ) ;
#15050=EDGE_CURVE ( 'NONE', #16578, #748, #8736, .T. ) ;
#15055=CIRCLE ( 'NONE', #9031, 84.99999999999997158 ) ;
#15059=EDGE_CURVE ( 'NONE', #2588, #12483, #3493, .T. ) ;
#15060=ADVANCED_FACE ( 'NONE', ( #10104 ), #10023, .F. ) ;
#15063=CIRCLE ( 'NONE', #5771, 4.695405383896011919 ) ;
#15071=CARTESIAN_POINT ( 'NONE',  ( 46.99999999999988631, 493.2350855268092573, -585.2659423243250103 ) ) ;
#15073=CARTESIAN_POINT ( 'NONE',  ( -45.00000000000000000, 473.6663340069158039, -548.2494070140132862 ) ) ;
#15079=DIRECTION ( 'NONE',  ( 1.000000000000000000, 0.000000000000000000, 0.000000000000000000 ) ) ;
#15085=CARTESIAN_POINT ( 'NONE',  ( 45.00000000000000000, 473.6663340069158039, -561.9448123979092315 ) ) ;
#15093=DIRECTION ( 'NONE',  ( 0.000000000000000000, 0.000000000000000000, -1.000000000000000000 ) ) ;
#15099=AXIS2_PLACEMENT_3D ( 'NONE', #13961, #2184, #6369 ) ;
#15100=DIRECTION ( 'NONE',  ( 0.000000000000000000, 0.000000000000000000, -1.000000000000000000 ) ) ;
#15101=VERTEX_POINT ( 'NONE', #3411 ) ;
#15114=ORIENTED_EDGE ( 'NONE', *, *, #15704, .F. ) ;
#15123=ORIENTED_EDGE ( 'NONE', *, *, #6337, .T. ) ;
#15127=CIRCLE ( 'NONE', #1139, 13.69540538389596485 ) ;
#15136=VECTOR ( 'NONE', #9443, 1000.000000000000000 ) ;
#15139=TOROIDAL_SURFACE ( 'NONE', #16787, 4.695405383895982609, 9.000000000000000000 ) ;
#15140=ORIENTED_EDGE ( 'NONE', *, *, #10235, .T. ) ;
#15145=DIRECTION ( 'NONE',  ( 1.000000000000000000, 0.000000000000000000, 0.000000000000000000 ) ) ;
#15151=DIRECTION ( 'NONE',  ( 1.000000000000000000, 0.000000000000000000, -0.000000000000000000 ) ) ;
#15152=AXIS2_PLACEMENT_3D ( 'NONE', #15533, #15776, #6399 ) ;
#15166=EDGE_CURVE ( 'NONE', #5839, #9380, #3911, .T. ) ;
#15181=DIRECTION ( 'NONE',  ( 1.000000000000000000, -0.000000000000000000, -0.000000000000000000 ) ) ;
#15183=AXIS2_PLACEMENT_3D ( 'NONE', #8972, #3647, #2509 ) ;
#15187=TOROIDAL_SURFACE ( 'NONE', #6119, 4.695405383895982609, 9.000000000000000000 ) ;
#15188=DIRECTION ( 'NONE',  ( 0.000000000000000000, 0.000000000000000000, -1.000000000000000000 ) ) ;
#15189=ORIENTED_EDGE ( 'NONE', *, *, #5724, .F. ) ;
#15190=DIRECTION ( 'NONE',  ( 0.000000000000000000, 0.000000000000000000, -1.000000000000000000 ) ) ;
#15192=CIRCLE ( 'NONE', #8045, 13.69540538389599682 ) ;
#15194=FACE_OUTER_BOUND ( 'NONE', #11089, .T. ) ;
#15196=ORIENTED_EDGE ( 'NONE', *, *, #9077, .T. ) ;
#15201=DIRECTION ( 'NONE',  ( -1.000000000000000000, 0.000000000000000000, 0.000000000000000000 ) ) ;
#15213=DIRECTION ( 'NONE',  ( 0.000000000000000000, 0.000000000000000000, -1.000000000000000000 ) ) ;
#15217=DIRECTION ( 'NONE',  ( 1.000000000000000000, 0.000000000000000000, 0.000000000000000000 ) ) ;
#15233=VERTEX_POINT ( 'NONE', #2279 ) ;
#15236=ORIENTED_EDGE ( 'NONE', *, *, #9537, .F. ) ;
#15241=CYLINDRICAL_SURFACE ( 'NONE', #7466, 13.69540538389601991 ) ;
#15244=CARTESIAN_POINT ( 'NONE',  ( 45.00000000000000000, 559.9933750504617365, -546.7230258972048205 ) ) ;
#15247=FACE_OUTER_BOUND ( 'NONE', #8670, .T. ) ;
#15249=AXIS2_PLACEMENT_3D ( 'NONE', #14806, #13686, #16343 ) ;
#15252=EDGE_LOOP ( 'NONE', ( #10178, #5754 ) ) ;
#15255=ORIENTED_EDGE ( 'NONE', *, *, #7721, .T. ) ;
#15258=CARTESIAN_POINT ( 'NONE',  ( 54.99999999999999289, 515.4878487013597805, -546.7230258972048205 ) ) ;
#15265=ORIENTED_EDGE ( 'NONE', *, *, #6507, .F. ) ;
#15270=PLANE ( 'NONE',  #11110 ) ;
#15273=AXIS2_PLACEMENT_3D ( 'NONE', #10697, #9250, #4272 ) ;
#15275=CIRCLE ( 'NONE', #7302, 84.99999999999997158 ) ;
#15279=EDGE_LOOP ( 'NONE', ( #9140, #10361, #2989, #2558 ) ) ;
#15296=CARTESIAN_POINT ( 'NONE',  ( -45.00000000000000000, 493.2350855268086320, -521.8755148539809170 ) ) ;
#15297=VERTEX_POINT ( 'NONE', #14482 ) ;
#15321=DIRECTION ( 'NONE',  ( 0.000000000000000000, 0.000000000000000000, 1.000000000000000000 ) ) ;
#15331=AXIS2_PLACEMENT_3D ( 'NONE', #15244, #9767, #4666 ) ;
#15344=DIRECTION ( 'NONE',  ( 0.000000000000000000, 0.000000000000000000, -1.000000000000000000 ) ) ;
#15348=CARTESIAN_POINT ( 'NONE',  ( 46.99999999999988631, 473.6663340069158039, -566.6402177818052905 ) ) ;
#15351=DIRECTION ( 'NONE',  ( 0.000000000000000000, 0.000000000000000000, -1.000000000000000000 ) ) ;
#15359=ORIENTED_EDGE ( 'NONE', *, *, #8324, .T. ) ;
#15365=DIRECTION ( 'NONE',  ( 0.000000000000000000, 0.000000000000000000, -1.000000000000000000 ) ) ;
#15367=VERTEX_POINT ( 'NONE', #11988 ) ;
#15371=ORIENTED_EDGE ( 'NONE', *, *, #9738, .T. ) ;
#15373=DIRECTION ( 'NONE',  ( 1.000000000000000000, -0.000000000000000000, 0.000000000000000000 ) ) ;
#15381=ADVANCED_FACE ( 'NONE', ( #2965 ), #2848, .T. ) ;
#15382=CARTESIAN_POINT ( 'NONE',  ( -55.99999999999989342, 559.9933750504617365, -546.7230258972048205 ) ) ;
#15384=AXIS2_PLACEMENT_3D ( 'NONE', #6665, #158, #13304 ) ;
#15386=DIRECTION ( 'NONE',  ( 0.000000000000000000, 0.000000000000000000, 1.000000000000000000 ) ) ;
#15390=EDGE_LOOP ( 'NONE', ( #15189, #8357, #1404, #274 ) ) ;
#15395=ADVANCED_FACE ( 'NONE', ( #13538 ), #15187, .T. ) ;
#15406=FACE_OUTER_BOUND ( 'NONE', #11612, .T. ) ;
#15408=DIRECTION ( 'NONE',  ( 1.000000000000000000, 0.000000000000000000, -0.000000000000000000 ) ) ;
#15410=ORIENTED_EDGE ( 'NONE', *, *, #10669, .F. ) ;
#15423=CIRCLE ( 'NONE', #8009, 13.69540538389601991 ) ;
#15428=CARTESIAN_POINT ( 'NONE',  ( 45.00000000000000000, 523.2161522479893847, -576.8570079137933817 ) ) ;
#15429=PLANE ( 'NONE',  #15803 ) ;
#15452=DIRECTION ( 'NONE',  ( 1.000000000000000000, 0.000000000000000000, 0.000000000000000000 ) ) ;
#15459=EDGE_CURVE ( 'NONE', #15233, #9156, #8617, .T. ) ;
#15460=FACE_OUTER_BOUND ( 'NONE', #10219, .T. ) ;
#15465=AXIS2_PLACEMENT_3D ( 'NONE', #8293, #2974, #16446 ) ;
#15466=CARTESIAN_POINT ( 'NONE',  ( 46.99999999999988631, 549.5810598491746077, -522.8108303813202156 ) ) ;
#15477=CIRCLE ( 'NONE', #9992, 4.695405383896011919 ) ;
#15480=VERTEX_POINT ( 'NONE', #16514 ) ;
#15481=EDGE_CURVE ( 'NONE', #14388, #12590, #10809, .T. ) ;
#15490=CARTESIAN_POINT ( 'NONE',  ( 54.99999999999999289, 515.4878487013597805, -546.7230258972048205 ) ) ;
#15493=AXIS2_PLACEMENT_3D ( 'NONE', #10640, #15873, #4112 ) ;
#15510=CARTESIAN_POINT ( 'NONE',  ( -46.99999999999988631, 523.2161522479893847, -604.2478186815853860 ) ) ;
#15518=CARTESIAN_POINT ( 'NONE',  ( -55.99999999999989342, 523.2161522479888163, -502.8936384967199729 ) ) ;
#15519=ORIENTED_EDGE ( 'NONE', *, *, #10847, .F. ) ;
#15526=CYLINDRICAL_SURFACE ( 'NONE', #6833, 13.69540538389601991 ) ;
#15528=ORIENTED_EDGE ( 'NONE', *, *, #15481, .F. ) ;
#15533=CARTESIAN_POINT ( 'NONE',  ( -46.99999999999988631, 523.2161522479888163, -502.8936384967199729 ) ) ;
#15534=ORIENTED_EDGE ( 'NONE', *, *, #11377, .T. ) ;
#15546=DIRECTION ( 'NONE',  ( -1.000000000000000000, -0.000000000000000000, -0.000000000000000000 ) ) ;
#15551=CIRCLE ( 'NONE', #3766, 13.69540538389601991 ) ;
#15564=AXIS2_PLACEMENT_3D ( 'NONE', #8151, #5657, #4202 ) ;
#15569=VERTEX_POINT ( 'NONE', #14991 ) ;
#15570=CYLINDRICAL_SURFACE ( 'NONE', #13506, 13.69540538389601991 ) ;
#15571=DIRECTION ( 'NONE',  ( 1.000000000000000000, 0.000000000000000000, 0.000000000000000000 ) ) ;
#15579=ORIENTED_EDGE ( 'NONE', *, *, #7725, .F. ) ;
#15580=CARTESIAN_POINT ( 'NONE',  ( 45.00000000000000000, 515.4878487013597805, -606.7230258972047068 ) ) ;
#15600=CARTESIAN_POINT ( 'NONE',  ( 55.99999999999989342, 559.9933750504617365, -546.7230258972048205 ) ) ;
#15602=DIRECTION ( 'NONE',  ( 1.000000000000000000, -0.000000000000000000, 0.000000000000000000 ) ) ;
#15618=CYLINDRICAL_SURFACE ( 'NONE', #14713, 187.4999999999998863 ) ;
#15623=EDGE_LOOP ( 'NONE', ( #7646, #9904 ) ) ;
#15626=DIRECTION ( 'NONE',  ( 1.000000000000000000, 0.000000000000000000, 0.000000000000000000 ) ) ;
#15635=AXIS2_PLACEMENT_3D ( 'NONE', #7926, #15836, #1500 ) ;
#15645=CARTESIAN_POINT ( 'NONE',  ( 55.99999999999989342, 473.6663340069157471, -531.5012393965008641 ) ) ;
#15646=DIRECTION ( 'NONE',  ( 0.000000000000000000, 0.000000000000000000, 1.000000000000000000 ) ) ;
#15672=EDGE_CURVE ( 'NONE', #3296, #13923, #11620, .T. ) ;
#15675=DIRECTION ( 'NONE',  ( 1.000000000000000000, -0.000000000000000000, -0.000000000000000000 ) ) ;
#15676=CARTESIAN_POINT ( 'NONE',  ( -55.99999999999989342, 549.5810598491749488, -575.3306267969850296 ) ) ;
#15683=ADVANCED_FACE ( 'NONE', ( #6358 ), #1232, .F. ) ;
#15692=VECTOR ( 'NONE', #6093, 1000.000000000000000 ) ;
#15694=ORIENTED_EDGE ( 'NONE', *, *, #3197, .F. ) ;
#15699=TOROIDAL_SURFACE ( 'NONE', #6640, 4.695405383895982609, 9.000000000000000000 ) ;
#15700=CARTESIAN_POINT ( 'NONE',  ( 54.99999999999999289, 515.4878487013597805, -359.2230258972048773 ) ) ;
#15704=EDGE_CURVE ( 'NONE', #5980, #15749, #10822, .T. ) ;
#15717=CARTESIAN_POINT ( 'NONE',  ( 46.99999999999988631, 473.6663340069157471, -531.5012393965008641 ) ) ;
#15720=ORIENTED_EDGE ( 'NONE', *, *, #16493, .F. ) ;
#15726=LINE ( 'NONE', #3977, #8905 ) ;
#15727=CIRCLE ( 'NONE', #3130, 13.69540538389601991 ) ;
#15731=CIRCLE ( 'NONE', #9708, 13.69540538389598794 ) ;
#15739=EDGE_CURVE ( 'NONE', #9277, #6058, #15477, .T. ) ;
#15749=VERTEX_POINT ( 'NONE', #9477 ) ;
#15760=LINE ( 'NONE', #9157, #13511 ) ;
#15767=CIRCLE ( 'NONE', #6419, 13.69540538389601991 ) ;
#15772=DIRECTION ( 'NONE',  ( 0.000000000000000000, 0.000000000000000000, 1.000000000000000000 ) ) ;
#15776=DIRECTION ( 'NONE',  ( -1.000000000000000000, 0.000000000000000000, 0.000000000000000000 ) ) ;
#15782=CARTESIAN_POINT ( 'NONE',  ( -55.99999999999989342, 549.5810598491746077, -518.1154249974242703 ) ) ;
#15787=CARTESIAN_POINT ( 'NONE',  ( 55.99999999999989342, 473.6663340069157471, -517.8058340126048051 ) ) ;
#15789=DIRECTION ( 'NONE',  ( 0.000000000000000000, 0.000000000000000000, -1.000000000000000000 ) ) ;
#15792=CARTESIAN_POINT ( 'NONE',  ( -55.99999999999989342, 523.2161522479893847, -604.2478186815853860 ) ) ;
#15796=CARTESIAN_POINT ( 'NONE',  ( 55.99999999999989342, 549.5810598491746077, -518.1154249974242703 ) ) ;
#15798=FACE_OUTER_BOUND ( 'NONE', #6347, .T. ) ;
#15801=CARTESIAN_POINT ( 'NONE',  ( 46.99999999999988631, 549.5810598491746077, -518.1154249974242703 ) ) ;
#15803=AXIS2_PLACEMENT_3D ( 'NONE', #2372, #13029, #11732 ) ;
#15817=ORIENTED_EDGE ( 'NONE', *, *, #14026, .F. ) ;
#15819=AXIS2_PLACEMENT_3D ( 'NONE', #16628, #10108, #15344 ) ;
#15826=CARTESIAN_POINT ( 'NONE',  ( 46.99999999999988631, 523.2161522479888163, -502.8936384967199729 ) ) ;
#15832=VERTEX_POINT ( 'NONE', #1653 ) ;
#15835=ORIENTED_EDGE ( 'NONE', *, *, #16843, .F. ) ;
#15836=DIRECTION ( 'NONE',  ( 0.000000000000000000, 1.000000000000000000, 1.224646799147353207E-16 ) ) ;
#15837=VERTEX_POINT ( 'NONE', #12135 ) ;
#15839=ORIENTED_EDGE ( 'NONE', *, *, #2921, .F. ) ;
#15840=CIRCLE ( 'NONE', #4335, 13.69540538389601991 ) ;
#15842=CARTESIAN_POINT ( 'NONE',  ( 46.99999999999988631, 559.9933750504617365, -560.4184312811007658 ) ) ;
#15843=DIRECTION ( 'NONE',  ( 0.000000000000000000, -1.000000000000000000, 0.000000000000000000 ) ) ;
#15846=LINE ( 'NONE', #11810, #6338 ) ;
#15849=LINE ( 'NONE', #405, #3202 ) ;
#15850=CARTESIAN_POINT ( 'NONE',  ( 46.99999999999988631, 559.9933750504617365, -533.0276205133087615 ) ) ;
#15851=DIRECTION ( 'NONE',  ( 1.000000000000000000, 0.000000000000000000, -0.000000000000000000 ) ) ;
#15852=DIRECTION ( 'NONE',  ( 0.000000000000000000, 0.000000000000000000, 1.000000000000000000 ) ) ;
#15855=CARTESIAN_POINT ( 'NONE',  ( 45.00000000000000000, 549.5810598491746077, -531.8108303813202156 ) ) ;
#15858=CARTESIAN_POINT ( 'NONE',  ( 45.00000000000000000, 473.6663340069158039, -548.2494070140132862 ) ) ;
#15873=DIRECTION ( 'NONE',  ( -1.000000000000000000, 0.000000000000000000, -0.000000000000000000 ) ) ;
#15879=DIRECTION ( 'NONE',  ( 1.000000000000000000, 0.000000000000000000, 0.000000000000000000 ) ) ;
#15890=PLANE ( 'NONE',  #416 ) ;
#15891=ORIENTED_EDGE ( 'NONE', *, *, #11917, .T. ) ;
#15897=ORIENTED_EDGE ( 'NONE', *, *, #13301, .T. ) ;
#15900=AXIS2_PLACEMENT_3D ( 'NONE', #8552, #4849, #7157 ) ;
#15902=AXIS2_PLACEMENT_3D ( 'NONE', #13727, #9698, #5733 ) ;
#15924=CYLINDRICAL_SURFACE ( 'NONE', #7701, 13.69540538389596485 ) ;
#15925=CARTESIAN_POINT ( 'NONE',  ( -46.99999999999988631, 559.9933750504617365, -546.7230258972048205 ) ) ;
#15929=AXIS2_PLACEMENT_3D ( 'NONE', #3246, #9778, #9597 ) ;
#15930=DIRECTION ( 'NONE',  ( 1.000000000000000000, 0.000000000000000000, 0.000000000000000000 ) ) ;
#15931=DIRECTION ( 'NONE',  ( 0.000000000000000000, 0.000000000000000000, -1.000000000000000000 ) ) ;
#15942=DIRECTION ( 'NONE',  ( 0.000000000000000000, -0.7625786632508376739, -0.6468954956981579629 ) ) ;
#15948=CARTESIAN_POINT ( 'NONE',  ( -55.99999999999989342, 523.2161522479893847, -576.8570079137933817 ) ) ;
#15949=EDGE_LOOP ( 'NONE', ( #4827, #10457 ) ) ;
#15950=DIRECTION ( 'NONE',  ( 1.000000000000000000, 0.000000000000000000, -0.000000000000000000 ) ) ;
#15959=CARTESIAN_POINT ( 'NONE',  ( 46.99999999999988631, 493.2350855268092573, -571.5705369404290650 ) ) ;
#15970=DIRECTION ( 'NONE',  ( 0.000000000000000000, 0.000000000000000000, 1.000000000000000000 ) ) ;
#15975=CARTESIAN_POINT ( 'NONE',  ( 46.99999999999988631, 493.2350855268086320, -503.4847040861888559 ) ) ;
#15981=AXIS2_PLACEMENT_3D ( 'NONE', #5463, #10711, #6669 ) ;
#15985=CIRCLE ( 'NONE', #3378, 9.000000000000007105 ) ;
#15990=EDGE_CURVE ( 'NONE', #11329, #4486, #12188, .T. ) ;
#16010=TOROIDAL_SURFACE ( 'NONE', #13275, 4.695405383895982609, 9.000000000000000000 ) ;
#16011=ORIENTED_EDGE ( 'NONE', *, *, #10660, .T. ) ;
#16021=AXIS2_PLACEMENT_3D ( 'NONE', #4392, #1558, #10733 ) ;
#16029=AXIS2_PLACEMENT_3D ( 'NONE', #1562, #104, #14446 ) ;
#16030=( GEOMETRIC_REPRESENTATION_CONTEXT ( 3 ) GLOBAL_UNCERTAINTY_ASSIGNED_CONTEXT ( ( #12205 ) ) GLOBAL_UNIT_ASSIGNED_CONTEXT ( ( #3381, #3551, #1914 ) ) REPRESENTATION_CONTEXT ( 'NONE', 'WORKASPACE' ) );
#16064=FACE_OUTER_BOUND ( 'NONE', #3262, .T. ) ;
#16065=ORIENTED_EDGE ( 'NONE', *, *, #10938, .F. ) ;
#16067=CARTESIAN_POINT ( 'NONE',  ( -45.00000000000000000, 523.2161522479888163, -502.8936384967199729 ) ) ;
#16068=DIRECTION ( 'NONE',  ( 0.000000000000000000, 0.000000000000000000, -1.000000000000000000 ) ) ;
#16088=EDGE_LOOP ( 'NONE', ( #550, #13184, #12585, #8379 ) ) ;
#16096=ORIENTED_EDGE ( 'NONE', *, *, #13038, .T. ) ;
#16103=CARTESIAN_POINT ( 'NONE',  ( 46.99999999999988631, 559.9933750504617365, -542.0276205133087615 ) ) ;
#16106=CIRCLE ( 'NONE', #8971, 13.69540538389599682 ) ;
#16107=DIRECTION ( 'NONE',  ( 1.000000000000000000, 0.000000000000000000, 0.000000000000000000 ) ) ;
#16114=DIRECTION ( 'NONE',  ( 0.000000000000000000, 0.000000000000000000, 1.000000000000000000 ) ) ;
#16115=CARTESIAN_POINT ( 'NONE',  ( -49.99999999999999289, 515.4878487013597805, -486.7230258972047636 ) ) ;
#16119=CARTESIAN_POINT ( 'NONE',  ( 45.00000000000000000, 523.2161522479888163, -502.8936384967199729 ) ) ;
#16125=DIRECTION ( 'NONE',  ( 0.000000000000000000, 0.6468954956981579629, -0.7625786632508376739 ) ) ;
#16128=AXIS2_PLACEMENT_3D ( 'NONE', #16136, #430, #4297 ) ;
#16130=ORIENTED_EDGE ( 'NONE', *, *, #1437, .F. ) ;
#16136=CARTESIAN_POINT ( 'NONE',  ( 55.99999999999989342, 493.2350855268092573, -585.2659423243250103 ) ) ;
#16145=ORIENTED_EDGE ( 'NONE', *, *, #12244, .F. ) ;
#16156=ORIENTED_EDGE ( 'NONE', *, *, #12980, .F. ) ;
#16174=ORIENTED_EDGE ( 'NONE', *, *, #10847, .T. ) ;
#16179=CARTESIAN_POINT ( 'NONE',  ( 45.00000000000000000, 523.2161522479893847, -590.5524132976893270 ) ) ;
#16192=ADVANCED_FACE ( 'NONE', ( #5322 ), #2871, .T. ) ;
#16196=LINE ( 'NONE', #9511, #11236 ) ;
#16198=EDGE_LOOP ( 'NONE', ( #4467, #447, #7366, #5910 ) ) ;
#16205=AXIS2_PLACEMENT_3D ( 'NONE', #7339, #12675, #11465 ) ;
#16212=CARTESIAN_POINT ( 'NONE',  ( -46.99999999999988631, 493.2350855268092573, -585.2659423243250103 ) ) ;
#16218=ORIENTED_EDGE ( 'NONE', *, *, #4061, .F. ) ;
#16221=DIRECTION ( 'NONE',  ( 0.000000000000000000, 0.000000000000000000, -1.000000000000000000 ) ) ;
#16231=CARTESIAN_POINT ( 'NONE',  ( -55.99999999999988631, 334.9272574771864015, -321.9943432880672276 ) ) ;
#16242=DIRECTION ( 'NONE',  ( 1.000000000000000000, 0.000000000000000000, 0.000000000000000000 ) ) ;
#16247=EDGE_LOOP ( 'NONE', ( #1053, #4081 ) ) ;
#16249=CIRCLE ( 'NONE', #12945, 4.695405383896011919 ) ;
#16250=LINE ( 'NONE', #3455, #15692 ) ;
#16257=ADVANCED_FACE ( 'NONE', ( #11765 ), #411, .T. ) ;
#16268=DIRECTION ( 'NONE',  ( 1.000000000000000000, 0.000000000000000000, 0.000000000000000000 ) ) ;
#16276=VECTOR ( 'NONE', #581, 1000.000000000000000 ) ;
#16280=CARTESIAN_POINT ( 'NONE',  ( -49.99999999999999289, 515.4878487013597805, -461.7230258972048205 ) ) ;
#16287=VERTEX_POINT ( 'NONE', #1464 ) ;
#16293=AXIS2_PLACEMENT_3D ( 'NONE', #7645, #9121, #6350 ) ;
#16300=CARTESIAN_POINT ( 'NONE',  ( 55.99999999999989342, 523.2161522479893847, -585.8570079137933817 ) ) ;
#16309=ORIENTED_EDGE ( 'NONE', *, *, #9537, .T. ) ;
#16310=CYLINDRICAL_SURFACE ( 'NONE', #7521, 13.69540538389601991 ) ;
#16315=EDGE_CURVE ( 'NONE', #3004, #6925, #836, .T. ) ;
#16316=EDGE_LOOP ( 'NONE', ( #13532, #4016, #4984, #15891 ) ) ;
#16336=ORIENTED_EDGE ( 'NONE', *, *, #8829, .F. ) ;
#16343=DIRECTION ( 'NONE',  ( 0.000000000000000000, 0.000000000000000000, -1.000000000000000000 ) ) ;
#16350=VECTOR ( 'NONE', #13564, 1000.000000000000000 ) ;
#16354=LINE ( 'NONE', #9833, #7450 ) ;
#16362=AXIS2_PLACEMENT_3D ( 'NONE', #8739, #2031, #10027 ) ;
#16376=CIRCLE ( 'NONE', #13874, 13.69540538389601636 ) ;
#16387=CARTESIAN_POINT ( 'NONE',  ( 46.99999999999988631, 549.5810598491749488, -589.0260321808809749 ) ) ;
#16393=( NAMED_UNIT ( * ) PLANE_ANGLE_UNIT ( ) SI_UNIT ( $, .RADIAN. ) );
#16400=DIRECTION ( 'NONE',  ( 0.000000000000000000, 0.000000000000000000, -1.000000000000000000 ) ) ;
#16403=ORIENTED_EDGE ( 'NONE', *, *, #15990, .T. ) ;
#16404=VERTEX_POINT ( 'NONE', #759 ) ;
#16414=EDGE_CURVE ( 'NONE', #3142, #14915, #7518, .T. ) ;
#16415=ORIENTED_EDGE ( 'NONE', *, *, #6459, .F. ) ;
#16421=CARTESIAN_POINT ( 'NONE',  ( 54.99999999999999289, 515.4878487013597805, -461.7230258972048205 ) ) ;
#16439=DIRECTION ( 'NONE',  ( -1.000000000000000000, 0.000000000000000000, 0.000000000000000000 ) ) ;
#16445=EDGE_CURVE ( 'NONE', #21, #13474, #5887, .T. ) ;
#16446=DIRECTION ( 'NONE',  ( 0.000000000000000000, 0.000000000000000000, -1.000000000000000000 ) ) ;
#16459=ORIENTED_EDGE ( 'NONE', *, *, #15672, .F. ) ;
#16475=ORIENTED_EDGE ( 'NONE', *, *, #14259, .F. ) ;
#16482=DIRECTION ( 'NONE',  ( 0.000000000000000000, 0.9848077530122062440, 0.1736481776669404620 ) ) ;
#16483=ORIENTED_EDGE ( 'NONE', *, *, #5798, .F. ) ;
#16484=ORIENTED_EDGE ( 'NONE', *, *, #13301, .F. ) ;
#16485=DIRECTION ( 'NONE',  ( 0.000000000000000000, 0.000000000000000000, -1.000000000000000000 ) ) ;
#16491=CARTESIAN_POINT ( 'NONE',  ( 49.99999999999999289, 515.4878487013597805, -546.7230258972048205 ) ) ;
#16493=EDGE_CURVE ( 'NONE', #7690, #7474, #5848, .T. ) ;
#16498=CARTESIAN_POINT ( 'NONE',  ( 46.99999999999988631, 493.2350855268086320, -521.8755148539809170 ) ) ;
#16502=ORIENTED_EDGE ( 'NONE', *, *, #2268, .F. ) ;
#16507=CIRCLE ( 'NONE', #7447, 9.000000000000007105 ) ;
#16512=CARTESIAN_POINT ( 'NONE',  ( -45.00000000000000000, 549.5810598491749488, -561.6352214130889706 ) ) ;
#16514=CARTESIAN_POINT ( 'NONE',  ( -45.00000000000000000, 515.4878487013597805, -606.7230258972047068 ) ) ;
#16521=DIRECTION ( 'NONE',  ( 1.000000000000000000, -0.000000000000000000, 0.000000000000000000 ) ) ;
#16555=CARTESIAN_POINT ( 'NONE',  ( 45.00000000000000000, 493.2350855268092573, -585.2659423243250103 ) ) ;
#16556=CARTESIAN_POINT ( 'NONE',  ( 55.99999999999989342, 473.6663340069158039, -561.9448123979092315 ) ) ;
#16560=ORIENTED_EDGE ( 'NONE', *, *, #7608, .T. ) ;
#16562=EDGE_CURVE ( 'NONE', #1196, #4760, #1476, .T. ) ;
#16568=AXIS2_PLACEMENT_3D ( 'NONE', #8999, #2451, #11651 ) ;
#16569=CYLINDRICAL_SURFACE ( 'NONE', #11746, 13.69540538389601991 ) ;
#16578=VERTEX_POINT ( 'NONE', #7763 ) ;
#16590=VERTEX_POINT ( 'NONE', #3829 ) ;
#16628=CARTESIAN_POINT ( 'NONE',  ( 45.00000000000000000, 473.6663340069157471, -531.5012393965008641 ) ) ;
#16631=CARTESIAN_POINT ( 'NONE',  ( -45.00000000000000000, 473.6663340069157471, -545.1966447803968094 ) ) ;
#16641=VECTOR ( 'NONE', #760, 1000.000000000000000 ) ;
#16643=DIRECTION ( 'NONE',  ( 0.000000000000000000, 0.000000000000000000, -1.000000000000000000 ) ) ;
#16644=DIRECTION ( 'NONE',  ( -1.000000000000000000, 0.000000000000000000, -0.000000000000000000 ) ) ;
#16647=AXIS2_PLACEMENT_3D ( 'NONE', #10507, #1319, #13355 ) ;
#16650=DIRECTION ( 'NONE',  ( 0.000000000000000000, 0.000000000000000000, -1.000000000000000000 ) ) ;
#16654=LINE ( 'NONE', #10055, #14754 ) ;
#16655=FACE_OUTER_BOUND ( 'NONE', #6193, .T. ) ;
#16659=CARTESIAN_POINT ( 'NONE',  ( 55.99999999999989342, 473.6663340069158039, -561.9448123979092315 ) ) ;
#16670=EDGE_LOOP ( 'NONE', ( #10230, #110, #8976, #13785 ) ) ;
#16673=ORIENTED_EDGE ( 'NONE', *, *, #9077, .F. ) ;
#16682=DIRECTION ( 'NONE',  ( 1.000000000000000000, 0.000000000000000000, 0.000000000000000000 ) ) ;
#16688=DIRECTION ( 'NONE',  ( 1.000000000000000000, -0.000000000000000000, -0.000000000000000000 ) ) ;
#16691=TOROIDAL_SURFACE ( 'NONE', #8482, 4.695405383895982609, 9.000000000000000000 ) ;
#16696=AXIS2_PLACEMENT_3D ( 'NONE', #8356, #4814, #9891 ) ;
#16703=CARTESIAN_POINT ( 'NONE',  ( -54.99999999999999289, 515.4878487013597805, -546.7230258972048205 ) ) ;
#16708=FACE_BOUND ( 'NONE', #15623, .T. ) ;
#16709=CYLINDRICAL_SURFACE ( 'NONE', #3356, 13.69540538389601991 ) ;
#16718=AXIS2_PLACEMENT_3D ( 'NONE', #6565, #15602, #3836 ) ;
#16722=EDGE_CURVE ( 'NONE', #7813, #1375, #10240, .T. ) ;
#16727=DIRECTION ( 'NONE',  ( 0.000000000000000000, 0.000000000000000000, -1.000000000000000000 ) ) ;
#16734=CIRCLE ( 'NONE', #8792, 8.999999999999952038 ) ;
#16744=CIRCLE ( 'NONE', #314, 9.000000000000007105 ) ;
#16752=FACE_OUTER_BOUND ( 'NONE', #3965, .T. ) ;
#16765=CARTESIAN_POINT ( 'NONE',  ( -46.99999999999988631, 473.6663340069157471, -526.8058340126048051 ) ) ;
#16787=AXIS2_PLACEMENT_3D ( 'NONE', #13063, #2739, #1286 ) ;
#16798=( GEOMETRIC_REPRESENTATION_CONTEXT ( 3 ) GLOBAL_UNCERTAINTY_ASSIGNED_CONTEXT ( ( #2281 ) ) GLOBAL_UNIT_ASSIGNED_CONTEXT ( ( #3261, #16393, #3595 ) ) REPRESENTATION_CONTEXT ( 'NONE', 'WORKASPACE' ) );
#16805=DIRECTION ( 'NONE',  ( 0.000000000000000000, 0.000000000000000000, 1.000000000000000000 ) ) ;
#16806=ORIENTED_EDGE ( 'NONE', *, *, #7608, .F. ) ;
#16815=LINE ( 'NONE', #5054, #4444 ) ;
#16817=AXIS2_PLACEMENT_3D ( 'NONE', #15717, #2406, #6426 ) ;
#16832=ORIENTED_EDGE ( 'NONE', *, *, #11006, .F. ) ;
#16839=ORIENTED_EDGE ( 'NONE', *, *, #6662, .T. ) ;
#16843=EDGE_CURVE ( 'NONE', #13853, #6401, #818, .T. ) ;
#16849=ORIENTED_EDGE ( 'NONE', *, *, #2425, .T. ) ;
#16851=AXIS2_PLACEMENT_3D ( 'NONE', #15801, #15879, #1632 ) ;
#16859=ORIENTED_EDGE ( 'NONE', *, *, #11959, .F. ) ;
#16877=TOROIDAL_SURFACE ( 'NONE', #3193, 4.695405383895982609, 9.000000000000000000 ) ;
#16891=DIRECTION ( 'NONE',  ( 0.000000000000000000, 0.6468954956981579629, -0.7625786632508376739 ) ) ;
#16893=CARTESIAN_POINT ( 'NONE',  ( 55.99999999999989342, 523.2161522479893847, -590.5524132976893270 ) ) ;
#16898=CIRCLE ( 'NONE', #15819, 13.69540538389601991 ) ;
#16902=EDGE_LOOP ( 'NONE', ( #360, #16415, #5766, #11265 ) ) ;
#16903=CYLINDRICAL_SURFACE ( 'NONE', #6690, 13.69540538389601991 ) ;
#16916=EDGE_CURVE ( 'NONE', #4130, #3064, #14360, .T. ) ;
#16920=AXIS2_PLACEMENT_3D ( 'NONE', #14422, #173, #6325 ) ;
#16926=EDGE_CURVE ( 'NONE', #1542, #5265, #15727, .T. ) ;
#16932=DIRECTION ( 'NONE',  ( -1.000000000000000000, 0.000000000000000000, -0.000000000000000000 ) ) ;
#16946=ORIENTED_EDGE ( 'NONE', *, *, #12568, .T. ) ;
#16954=ADVANCED_FACE ( 'NONE', ( #2344 ), #2424, .T. ) ;
#16955=EDGE_CURVE ( 'NONE', #8117, #15832, #11092, .T. ) ;
#16959=CIRCLE ( 'NONE', #1328, 25.00000000000002132 ) ;
#16961=PLANE ( 'NONE',  #11300 ) ;
ENDSEC;
END-ISO-10303-21;
